ISO-10303-21;
HEADER;
FILE_DESCRIPTION (('STEP AP214'),
    '1' );
FILE_NAME ('circlip for shafts normal_din_Circlip DIN 471 - 8 x 0.8.step',
    '2026-10-31T03:44:21',
    ( '' ),
    ( '' ),
    'SwSTEP 2.0',
    'SolidWorks 2026',
    '' );
FILE_SCHEMA (( 'AUTOMOTIVE_DESIGN' ));
ENDSEC;

DATA;
#20=LINE ( 'NONE', #7849, #12198 ) ;
#28=FACE_OUTER_BOUND ( 'NONE', #18793, .T. ) ;
#58=EDGE_CURVE ( 'NONE', #17997, #75, #9295, .T. ) ;
#72=DIRECTION ( 'NONE',  ( -0.000000000000000000, -0.000000000000000000, 1.000000000000000000 ) ) ;
#75=VERTEX_POINT ( 'NONE', #7374 ) ;
#102=EDGE_CURVE ( 'NONE', #16449, #12595, #15014, .T. ) ;
#115=CARTESIAN_POINT ( 'NONE',  ( 0.000000000000000000, 0.000000000000000000, 0.000000000000000000 ) ) ;
#148=CARTESIAN_POINT ( 'NONE',  ( -0.2000000000000000111, -6.997142273814360713, -0.8000000000000000444 ) ) ;
#170=DIRECTION ( 'NONE',  ( 0.000000000000000000, -1.000000000000000000, -0.000000000000000000 ) ) ;
#173=CARTESIAN_POINT ( 'NONE',  ( 0.000000000000000000, 0.000000000000000000, -0.8000000000000000444 ) ) ;
#174=ADVANCED_FACE ( 'NONE', ( #9593 ), #15208, .F. ) ;
#205=AXIS2_PLACEMENT_3D ( 'NONE', #2952, #1472, #19344 ) ;
#210=CARTESIAN_POINT ( 'NONE',  ( -1.398397006336996817, -6.091550361990593743, -0.8000000000000000444 ) ) ;
#215=CYLINDRICAL_SURFACE ( 'NONE', #17154, 2.447112362156698140 ) ;
#231=DIRECTION ( 'NONE',  ( 1.000000000000000000, 0.000000000000000000, 0.000000000000000000 ) ) ;
#245=ORIENTED_EDGE ( 'NONE', *, *, #9904, .T. ) ;
#246=ORIENTED_EDGE ( 'NONE', *, *, #5677, .F. ) ;
#252=ORIENTED_EDGE ( 'NONE', *, *, #14423, .F. ) ;
#288=UNCERTAINTY_MEASURE_WITH_UNIT (LENGTH_MEASURE( 1.000000000000000082E-05 ), #7865, 'distance_accuracy_value', 'NONE');
#328=FILL_AREA_STYLE_COLOUR ( '', #15956 ) ;
#379=CARTESIAN_POINT ( 'NONE',  ( -1.398397006336996817, -6.091550361990593743, -0.8000000000000000444 ) ) ;
#401=AXIS2_PLACEMENT_3D ( 'NONE', #6427, #3787, #15746 ) ;
#406=EDGE_CURVE ( 'NONE', #12668, #6480, #5479, .T. ) ;
#419=CARTESIAN_POINT ( 'NONE',  ( -2.141980652367355020, -6.189445006155633422, 0.000000000000000000 ) ) ;
#436=CARTESIAN_POINT ( 'NONE',  ( 1.000000000000000000, -5.408326913195983465, -0.8000000000000000444 ) ) ;
#450=ORIENTED_EDGE ( 'NONE', *, *, #569, .F. ) ;
#460=ADVANCED_FACE ( 'NONE', ( #14594 ), #1653, .F. ) ;
#482=VECTOR ( 'NONE', #1590, 1000.000000000000000 ) ;
#488=VERTEX_POINT ( 'NONE', #18125 ) ;
#500=AXIS2_PLACEMENT_3D ( 'NONE', #15472, #12246, #13989 ) ;
#537=ORIENTED_EDGE ( 'NONE', *, *, #13110, .T. ) ;
#569=EDGE_CURVE ( 'NONE', #7216, #5656, #16454, .T. ) ;
#610=VECTOR ( 'NONE', #15203, 1000.000000000000000 ) ;
#612=DIRECTION ( 'NONE',  ( -1.000000000000000000, 0.000000000000000000, 0.000000000000000000 ) ) ;
#627=CIRCLE ( 'NONE', #7209, 0.5999999999999998668 ) ;
#635=EDGE_CURVE ( 'NONE', #6724, #14776, #17314, .T. ) ;
#647=CARTESIAN_POINT ( 'NONE',  ( -4.747884751462026820, -5.143694235355983579, -0.8000000000000000444 ) ) ;
#678=LINE ( 'NONE', #3432, #2073 ) ;
#724=FACE_OUTER_BOUND ( 'NONE', #3141, .T. ) ;
#731=CARTESIAN_POINT ( 'NONE',  ( 0.9999999999999997780, -6.008326913195983998, 0.000000000000000000 ) ) ;
#742=CARTESIAN_POINT ( 'NONE',  ( -0.1085714285714285687, -3.798448662927795372, -0.8000000000000000444 ) ) ;
#772=EDGE_CURVE ( 'NONE', #6867, #16920, #13086, .T. ) ;
#794=CIRCLE ( 'NONE', #14566, 7.000000000000000000 ) ;
#803=EDGE_LOOP ( 'NONE', ( #2536, #10777, #7323, #12200 ) ) ;
#816=LINE ( 'NONE', #6596, #2010 ) ;
#821=CARTESIAN_POINT ( 'NONE',  ( 2.141980652367355464, -6.189445006155633422, -0.8000000000000000444 ) ) ;
#860=CIRCLE ( 'NONE', #5248, 2.447112362156698140 ) ;
#893=EDGE_CURVE ( 'NONE', #7333, #12819, #16525, .T. ) ;
#900=CARTESIAN_POINT ( 'NONE',  ( 1.566204647097437341, -6.822536405429464601, -0.8000000000000000444 ) ) ;
#935=LINE ( 'NONE', #14456, #16661 ) ;
#993=CARTESIAN_POINT ( 'NONE',  ( 1.398397006336996817, -6.091550361990593743, 0.000000000000000000 ) ) ;
#1031=VERTEX_POINT ( 'NONE', #3755 ) ;
#1048=CYLINDRICAL_SURFACE ( 'NONE', #2822, 7.000000000000000000 ) ;
#1068=DIRECTION ( 'NONE',  ( 1.000000000000000000, 0.000000000000000000, 0.000000000000000000 ) ) ;
#1147=PLANE ( 'NONE',  #16880 ) ;
#1161=DIRECTION ( 'NONE',  ( 0.9914448613738103822, -0.1305261922200521840, 0.000000000000000000 ) ) ;
#1197=EDGE_CURVE ( 'NONE', #7823, #8408, #14228, .T. ) ;
#1198=AXIS2_PLACEMENT_3D ( 'NONE', #1893, #7863, #13838 ) ;
#1206=DIRECTION ( 'NONE',  ( 0.000000000000000000, 0.000000000000000000, 1.000000000000000000 ) ) ;
#1218=EDGE_LOOP ( 'NONE', ( #16081, #537, #7795, #14958 ) ) ;
#1286=CARTESIAN_POINT ( 'NONE',  ( 0.000000000000000000, 0.4273491293402468805, -0.8000000000000000444 ) ) ;
#1295=DIRECTION ( 'NONE',  ( 0.000000000000000000, 0.000000000000000000, 1.000000000000000000 ) ) ;
#1307=DIRECTION ( 'NONE',  ( 1.000000000000000000, 0.000000000000000000, 0.000000000000000000 ) ) ;
#1325=ORIENTED_EDGE ( 'NONE', *, *, #14048, .F. ) ;
#1326=CARTESIAN_POINT ( 'NONE',  ( -4.747884751462026820, -5.143694235355983579, 0.000000000000000000 ) ) ;
#1329=DIRECTION ( 'NONE',  ( 1.000000000000000000, 0.000000000000000000, 0.000000000000000000 ) ) ;
#1339=ORIENTED_EDGE ( 'NONE', *, *, #1197, .T. ) ;
#1370=ORIENTED_EDGE ( 'NONE', *, *, #9854, .F. ) ;
#1385=CYLINDRICAL_SURFACE ( 'NONE', #7142, 2.447112362156698140 ) ;
#1393=DIRECTION ( 'NONE',  ( 0.02857142857142857401, 0.9995917534020515305, -0.000000000000000000 ) ) ;
#1395=VECTOR ( 'NONE', #15016, 1000.000000000000000 ) ;
#1396=PLANE ( 'NONE',  #9068 ) ;
#1402=DIRECTION ( 'NONE',  ( 0.000000000000000000, 0.000000000000000000, 1.000000000000000000 ) ) ;
#1416=EDGE_CURVE ( 'NONE', #1616, #6480, #11976, .T. ) ;
#1419=CYLINDRICAL_SURFACE ( 'NONE', #19350, 4.872650870659752442 ) ;
#1424=ADVANCED_FACE ( 'NONE', ( #7376 ), #215, .F. ) ;
#1468=CARTESIAN_POINT ( 'NONE',  ( -0.1717365941144614327, -6.008326913195983998, 0.000000000000000000 ) ) ;
#1472=DIRECTION ( 'NONE',  ( 0.000000000000000000, 0.000000000000000000, 1.000000000000000000 ) ) ;
#1510=ADVANCED_FACE ( 'NONE', ( #28 ), #13450, .T. ) ;
#1565=VERTEX_POINT ( 'NONE', #4445 ) ;
#1590=DIRECTION ( 'NONE',  ( -1.000000000000000000, -0.000000000000000000, -0.000000000000000000 ) ) ;
#1606=EDGE_CURVE ( 'NONE', #15143, #8758, #16211, .T. ) ;
#1615=LINE ( 'NONE', #4924, #2513 ) ;
#1616=VERTEX_POINT ( 'NONE', #12557 ) ;
#1622=ORIENTED_EDGE ( 'NONE', *, *, #2088, .F. ) ;
#1653=PLANE ( 'NONE',  #14230 ) ;
#1656=DIRECTION ( 'NONE',  ( -0.000000000000000000, -0.000000000000000000, 1.000000000000000000 ) ) ;
#1662=ORIENTED_EDGE ( 'NONE', *, *, #635, .F. ) ;
#1678=DIRECTION ( 'NONE',  ( 1.000000000000000000, 0.000000000000000000, -0.000000000000000000 ) ) ;
#1691=DIRECTION ( 'NONE',  ( -0.000000000000000000, -0.000000000000000000, -1.000000000000000000 ) ) ;
#1725=LINE ( 'NONE', #2186, #13300 ) ;
#1734=EDGE_CURVE ( 'NONE', #4109, #9092, #4630, .T. ) ;
#1737=ORIENTED_EDGE ( 'NONE', *, *, #9233, .F. ) ;
#1756=DIRECTION ( 'NONE',  ( 1.000000000000000000, 0.000000000000000000, 0.000000000000000000 ) ) ;
#1759=ORIENTED_EDGE ( 'NONE', *, *, #16169, .F. ) ;
#1762=DIRECTION ( 'NONE',  ( 0.02857142857142857401, -0.9995917534020515305, 0.000000000000000000 ) ) ;
#1805=CARTESIAN_POINT ( 'NONE',  ( 1.398397006336996817, -6.091550361990593743, -0.8000000000000000444 ) ) ;
#1840=STYLED_ITEM('',(#19468),#14915);
#1853=EDGE_CURVE ( 'NONE', #13632, #5656, #14274, .T. ) ;
#1893=CARTESIAN_POINT ( 'NONE',  ( 1.000000000000000000, -5.408326913195983465, -0.8000000000000000444 ) ) ;
#1895=PRESENTATION_STYLE_ASSIGNMENT (( #15317 ) ) ;
#1914=EDGE_CURVE ( 'NONE', #75, #14471, #5837, .T. ) ;
#1933=ORIENTED_EDGE ( 'NONE', *, *, #17501, .F. ) ;
#1956=ADVANCED_FACE ( 'NONE', ( #7351 ), #17961, .F. ) ;
#1976=EDGE_CURVE ( 'NONE', #1616, #7030, #14586, .T. ) ;
#2010=VECTOR ( 'NONE', #1656, 1000.000000000000000 ) ;
#2015=EDGE_CURVE ( 'NONE', #8758, #2066, #17745, .T. ) ;
#2050=PRODUCT_DEFINITION_CONTEXT ( 'detailed design', #12402, 'design' ) ;
#2066=VERTEX_POINT ( 'NONE', #16678 ) ;
#2073=VECTOR ( 'NONE', #6267, 1000.000000000000000 ) ;
#2088=EDGE_CURVE ( 'NONE', #488, #16920, #678, .T. ) ;
#2091=ORIENTED_EDGE ( 'NONE', *, *, #12568, .F. ) ;
#2092=LINE ( 'NONE', #17194, #5521 ) ;
#2106=EDGE_LOOP ( 'NONE', ( #1339, #12159, #11336, #17606 ) ) ;
#2152=EDGE_CURVE ( 'NONE', #14471, #2159, #17422, .T. ) ;
#2159=VERTEX_POINT ( 'NONE', #9782 ) ;
#2186=CARTESIAN_POINT ( 'NONE',  ( 0.9999999999999997780, -6.008326913195983998, -0.8000000000000000444 ) ) ;
#2195=EDGE_CURVE ( 'NONE', #7333, #6135, #9967, .T. ) ;
#2203=DIRECTION ( 'NONE',  ( 0.000000000000000000, 0.000000000000000000, 1.000000000000000000 ) ) ;
#2210=CIRCLE ( 'NONE', #9427, 3.799999999999999378 ) ;
#2290=ORIENTED_EDGE ( 'NONE', *, *, #1606, .T. ) ;
#2350=ORIENTED_EDGE ( 'NONE', *, *, #15140, .F. ) ;
#2391=CARTESIAN_POINT ( 'NONE',  ( -1.000000000000000000, -5.408326913195983465, -0.8000000000000000444 ) ) ;
#2395=CARTESIAN_POINT ( 'NONE',  ( -0.1374368770859596967, -4.808326913195983821, -0.8000000000000000444 ) ) ;
#2399=FACE_OUTER_BOUND ( 'NONE', #11479, .T. ) ;
#2405=DIRECTION ( 'NONE',  ( 1.000000000000000000, 0.000000000000000000, 0.000000000000000000 ) ) ;
#2442=DIRECTION ( 'NONE',  ( 1.000000000000000000, 0.000000000000000000, 0.000000000000000000 ) ) ;
#2449=LINE ( 'NONE', #8403, #3298 ) ;
#2486=SHAPE_REPRESENTATION_RELATIONSHIP ( 'NONE' , 'NONE' ,  #13919, #6604 ) ;
#2492=CARTESIAN_POINT ( 'NONE',  ( 0.000000000000000000, 0.4273491293402468805, -0.8000000000000000444 ) ) ;
#2513=VECTOR ( 'NONE', #10893, 1000.000000000000000 ) ;
#2521=CIRCLE ( 'NONE', #19110, 0.5999999999999999778 ) ;
#2535=CARTESIAN_POINT ( 'NONE',  ( 0.000000000000000000, 0.000000000000000000, -0.8000000000000000444 ) ) ;
#2536=ORIENTED_EDGE ( 'NONE', *, *, #9904, .F. ) ;
#2554=VECTOR ( 'NONE', #19275, 1000.000000000000114 ) ;
#2565=AXIS2_PLACEMENT_3D ( 'NONE', #6890, #2203, #2405 ) ;
#2566=LINE ( 'NONE', #8524, #7436 ) ;
#2618=VERTEX_POINT ( 'NONE', #18972 ) ;
#2668=DIRECTION ( 'NONE',  ( 0.000000000000000000, 0.000000000000000000, 1.000000000000000000 ) ) ;
#2669=VECTOR ( 'NONE', #9989, 1000.000000000000000 ) ;
#2674=DIRECTION ( 'NONE',  ( 0.000000000000000000, -0.000000000000000000, 1.000000000000000000 ) ) ;
#2778=CARTESIAN_POINT ( 'NONE',  ( 0.000000000000000000, 0.000000000000000000, 0.000000000000000000 ) ) ;
#2822=AXIS2_PLACEMENT_3D ( 'NONE', #2535, #7015, #16146 ) ;
#2871=CARTESIAN_POINT ( 'NONE',  ( 0.000000000000000000, 0.000000000000000000, 0.000000000000000000 ) ) ;
#2952=CARTESIAN_POINT ( 'NONE',  ( 0.000000000000000000, 0.4273491293402468805, 0.000000000000000000 ) ) ;
#2956=AXIS2_PLACEMENT_3D ( 'NONE', #173, #6148, #18677 ) ;
#2968=CARTESIAN_POINT ( 'NONE',  ( -0.1085714285714285687, -3.798448662927795372, -0.8000000000000000444 ) ) ;
#3014=CIRCLE ( 'NONE', #13941, 3.799999999999999378 ) ;
#3061=VECTOR ( 'NONE', #15468, 1000.000000000000000 ) ;
#3141=EDGE_LOOP ( 'NONE', ( #14070, #5455, #11633, #16977 ) ) ;
#3168=CIRCLE ( 'NONE', #16306, 3.799999999999999378 ) ;
#3197=VECTOR ( 'NONE', #1402, 1000.000000000000000 ) ;
#3203=ADVANCED_FACE ( 'NONE', ( #5736 ), #17617, .T. ) ;
#3226=ORIENTED_EDGE ( 'NONE', *, *, #14676, .F. ) ;
#3255=CYLINDRICAL_SURFACE ( 'NONE', #11433, 0.7500000000000002220 ) ;
#3292=EDGE_LOOP ( 'NONE', ( #10273, #10369, #13678, #17207 ) ) ;
#3298=VECTOR ( 'NONE', #3815, 1000.000000000000114 ) ;
#3309=CARTESIAN_POINT ( 'NONE',  ( 2.141980652367355464, -6.189445006155633422, -0.8000000000000000444 ) ) ;
#3430=PLANE ( 'NONE',  #8912 ) ;
#3432=CARTESIAN_POINT ( 'NONE',  ( -1.000000000000000222, -4.808326913195983821, -0.8000000000000000444 ) ) ;
#3434=CARTESIAN_POINT ( 'NONE',  ( -3.799999999999999378, 4.653657836759941744E-16, 0.000000000000000000 ) ) ;
#3449=DIRECTION ( 'NONE',  ( 1.000000000000000000, 0.000000000000000000, 0.000000000000000000 ) ) ;
#3492=VERTEX_POINT ( 'NONE', #18199 ) ;
#3493=CARTESIAN_POINT ( 'NONE',  ( -0.1085714285714285687, -3.798448662927795372, -0.8000000000000000444 ) ) ;
#3526=EDGE_CURVE ( 'NONE', #5579, #13512, #3568, .T. ) ;
#3532=ADVANCED_FACE ( 'NONE', ( #12288 ), #6488, .T. ) ;
#3568=CIRCLE ( 'NONE', #17674, 3.799999999999999378 ) ;
#3598=VERTEX_POINT ( 'NONE', #15328 ) ;
#3654=DIRECTION ( 'NONE',  ( 0.000000000000000000, 0.000000000000000000, 1.000000000000000000 ) ) ;
#3725=AXIS2_PLACEMENT_3D ( 'NONE', #13000, #5542, #12708 ) ;
#3730=MECHANICAL_DESIGN_GEOMETRIC_PRESENTATION_REPRESENTATION('',(#14055),#11233);
#3746=CARTESIAN_POINT ( 'NONE',  ( 0.1999999999999985678, -6.997142273814360713, -0.8000000000000000444 ) ) ;
#3755=CARTESIAN_POINT ( 'NONE',  ( 0.1999999999999985678, -6.997142273814360713, 0.000000000000000000 ) ) ;
#3768=ORIENTED_EDGE ( 'NONE', *, *, #15402, .T. ) ;
#3787=DIRECTION ( 'NONE',  ( 0.000000000000000000, 0.000000000000000000, 1.000000000000000000 ) ) ;
#3815=DIRECTION ( 'NONE',  ( 0.02857142857142857401, -0.9995917534020515305, 0.000000000000000000 ) ) ;
#3872=ADVANCED_FACE ( 'NONE', ( #14819 ), #14720, .T. ) ;
#3888=EDGE_CURVE ( 'NONE', #8758, #75, #13252, .T. ) ;
#3889=CARTESIAN_POINT ( 'NONE',  ( -4.872650870659752442, 0.4273491293402474911, -0.8000000000000000444 ) ) ;
#3898=CARTESIAN_POINT ( 'NONE',  ( 0.1085714285714285687, -3.798448662927795372, 0.000000000000000000 ) ) ;
#4007=AXIS2_PLACEMENT_3D ( 'NONE', #5808, #17777, #10304 ) ;
#4019=ORIENTED_EDGE ( 'NONE', *, *, #13243, .T. ) ;
#4032=CARTESIAN_POINT ( 'NONE',  ( 0.000000000000000000, 0.000000000000000000, -0.8000000000000000444 ) ) ;
#4047=ORIENTED_EDGE ( 'NONE', *, *, #12958, .T. ) ;
#4073=ORIENTED_EDGE ( 'NONE', *, *, #3526, .T. ) ;
#4084=AXIS2_PLACEMENT_3D ( 'NONE', #18600, #13954, #7981 ) ;
#4109=VERTEX_POINT ( 'NONE', #16888 ) ;
#4129=DIRECTION ( 'NONE',  ( -0.000000000000000000, -0.000000000000000000, -1.000000000000000000 ) ) ;
#4143=CARTESIAN_POINT ( 'NONE',  ( 0.1717365941144614327, -6.008326913195983998, 0.000000000000000000 ) ) ;
#4249=EDGE_CURVE ( 'NONE', #12819, #12668, #11364, .T. ) ;
#4306=AXIS2_PLACEMENT_3D ( 'NONE', #742, #6522, #12802 ) ;
#4323=ORIENTED_EDGE ( 'NONE', *, *, #15886, .F. ) ;
#4324=LINE ( 'NONE', #18063, #6498 ) ;
#4376=ORIENTED_EDGE ( 'NONE', *, *, #11157, .F. ) ;
#4407=EDGE_LOOP ( 'NONE', ( #18429, #15682, #2350, #14629 ) ) ;
#4421=DIRECTION ( 'NONE',  ( 0.000000000000000000, 0.000000000000000000, 1.000000000000000000 ) ) ;
#4445=CARTESIAN_POINT ( 'NONE',  ( -1.000000000000000222, -4.808326913195983821, -0.8000000000000000444 ) ) ;
#4456=ORIENTED_EDGE ( 'NONE', *, *, #16591, .F. ) ;
#4491=ADVANCED_FACE ( 'NONE', ( #16866 ), #3430, .F. ) ;
#4575=CARTESIAN_POINT ( 'NONE',  ( 0.1717365941144614327, -6.008326913195983998, -0.8000000000000000444 ) ) ;
#4629=DIRECTION ( 'NONE',  ( 0.02857142857142857401, 0.9995917534020515305, -0.000000000000000000 ) ) ;
#4630=CIRCLE ( 'NONE', #7753, 7.000000000000000000 ) ;
#4694=CARTESIAN_POINT ( 'NONE',  ( -1.566204647097437563, -6.822536405429463713, 0.000000000000000000 ) ) ;
#4697=EDGE_LOOP ( 'NONE', ( #1759, #17403, #16084, #19108, #3768, #7361, #14692, #7390, #12661, #11357, #8074, #8079, #15171, #17463, #15535, #12226, #4943, #4323, #15579, #12090, #11431, #12510, #17356, #4073, #11425 ) ) ;
#4722=ORIENTED_EDGE ( 'NONE', *, *, #4865, .F. ) ;
#4780=CARTESIAN_POINT ( 'NONE',  ( 0.9999999999999997780, -6.008326913195983998, -0.8000000000000000444 ) ) ;
#4802=UNCERTAINTY_MEASURE_WITH_UNIT (LENGTH_MEASURE( 1.000000000000000082E-05 ), #11254, 'distance_accuracy_value', 'NONE');
#4806=DIRECTION ( 'NONE',  ( 0.000000000000000000, -1.000000000000000000, -0.000000000000000000 ) ) ;
#4817=FACE_OUTER_BOUND ( 'NONE', #12300, .T. ) ;
#4818=LINE ( 'NONE', #10781, #610 ) ;
#4838=EDGE_CURVE ( 'NONE', #3598, #16920, #2449, .T. ) ;
#4850=ADVANCED_FACE ( 'NONE', ( #10259 ), #8604, .T. ) ;
#4865=EDGE_CURVE ( 'NONE', #8472, #7823, #18028, .T. ) ;
#4871=VECTOR ( 'NONE', #10193, 1000.000000000000000 ) ;
#4881=EDGE_LOOP ( 'NONE', ( #3226, #5476, #14041, #10011 ) ) ;
#4890=CARTESIAN_POINT ( 'NONE',  ( 3.799999999999999378, 0.000000000000000000, -0.8000000000000000444 ) ) ;
#4924=CARTESIAN_POINT ( 'NONE',  ( -1.000000000000000222, -4.808326913195983821, 0.000000000000000000 ) ) ;
#4932=CARTESIAN_POINT ( 'NONE',  ( -0.1717365941144614605, -6.008326913195983998, -0.8000000000000000444 ) ) ;
#4943=ORIENTED_EDGE ( 'NONE', *, *, #4865, .T. ) ;
#4983=DIRECTION ( 'NONE',  ( 0.000000000000000000, 0.000000000000000000, 1.000000000000000000 ) ) ;
#4985=DIRECTION ( 'NONE',  ( 0.000000000000000000, 0.000000000000000000, -1.000000000000000000 ) ) ;
#5007=CARTESIAN_POINT ( 'NONE',  ( 4.747884751462026820, -5.143694235355983579, -0.8000000000000000444 ) ) ;
#5051=CARTESIAN_POINT ( 'NONE',  ( 1.599999999999999867, -5.408326913195983465, -0.8000000000000000444 ) ) ;
#5075=EDGE_CURVE ( 'NONE', #488, #10416, #816, .T. ) ;
#5106=DIRECTION ( 'NONE',  ( 0.000000000000000000, 0.000000000000000000, 1.000000000000000000 ) ) ;
#5181=LINE ( 'NONE', #10970, #10933 ) ;
#5183=ORIENTED_EDGE ( 'NONE', *, *, #7411, .T. ) ;
#5188=ADVANCED_FACE ( 'NONE', ( #12579 ), #12675, .F. ) ;
#5201=ADVANCED_FACE ( 'NONE', ( #2399 ), #11387, .F. ) ;
#5225=EDGE_LOOP ( 'NONE', ( #1325, #450, #9826, #16567 ) ) ;
#5228=ORIENTED_EDGE ( 'NONE', *, *, #8449, .F. ) ;
#5248=AXIS2_PLACEMENT_3D ( 'NONE', #647, #6911, #12900 ) ;
#5279=ORIENTED_EDGE ( 'NONE', *, *, #1914, .F. ) ;
#5352=VECTOR ( 'NONE', #19385, 1000.000000000000000 ) ;
#5359=PLANE ( 'NONE',  #3725 ) ;
#5386=( NAMED_UNIT ( * ) SI_UNIT ( $, .STERADIAN. ) SOLID_ANGLE_UNIT ( ) );
#5446=EDGE_CURVE ( 'NONE', #14776, #16413, #13452, .T. ) ;
#5454=DIRECTION ( 'NONE',  ( 0.000000000000000000, -0.000000000000000000, 1.000000000000000000 ) ) ;
#5455=ORIENTED_EDGE ( 'NONE', *, *, #7882, .F. ) ;
#5476=ORIENTED_EDGE ( 'NONE', *, *, #16237, .F. ) ;
#5479=CIRCLE ( 'NONE', #7979, 0.7500000000000002220 ) ;
#5488=CIRCLE ( 'NONE', #14238, 3.799999999999999378 ) ;
#5521=VECTOR ( 'NONE', #16806, 1000.000000000000114 ) ;
#5526=CARTESIAN_POINT ( 'NONE',  ( 0.9999999999999997780, -6.008326913195983998, -0.8000000000000000444 ) ) ;
#5542=DIRECTION ( 'NONE',  ( -0.9914448613738103822, -0.1305261922200521840, 0.000000000000000000 ) ) ;
#5568=VECTOR ( 'NONE', #12577, 1000.000000000000000 ) ;
#5576=EDGE_CURVE ( 'NONE', #2066, #6724, #10372, .T. ) ;
#5579=VERTEX_POINT ( 'NONE', #15702 ) ;
#5656=VERTEX_POINT ( 'NONE', #14013 ) ;
#5666=DIRECTION ( 'NONE',  ( 0.1305261922200521840, 0.9914448613738103822, 0.000000000000000000 ) ) ;
#5677=EDGE_CURVE ( 'NONE', #6135, #12668, #16791, .T. ) ;
#5679=( NAMED_UNIT ( * ) PLANE_ANGLE_UNIT ( ) SI_UNIT ( $, .RADIAN. ) );
#5694=EDGE_CURVE ( 'NONE', #8944, #2618, #2210, .T. ) ;
#5730=ADVANCED_FACE ( 'NONE', ( #16091 ), #8725, .F. ) ;
#5736=FACE_OUTER_BOUND ( 'NONE', #7293, .T. ) ;
#5751=ORIENTED_EDGE ( 'NONE', *, *, #7832, .F. ) ;
#5757=FACE_OUTER_BOUND ( 'NONE', #803, .T. ) ;
#5770=CARTESIAN_POINT ( 'NONE',  ( 1.566204647097437341, -6.822536405429464601, 0.000000000000000000 ) ) ;
#5804=DIRECTION ( 'NONE',  ( 0.000000000000000000, 0.000000000000000000, 1.000000000000000000 ) ) ;
#5808=CARTESIAN_POINT ( 'NONE',  ( 0.1085714285714285687, -3.798448662927795372, -0.8000000000000000444 ) ) ;
#5814=LINE ( 'NONE', #16316, #2554 ) ;
#5833=DIRECTION ( 'NONE',  ( 0.000000000000000000, 0.000000000000000000, -1.000000000000000000 ) ) ;
#5837=CIRCLE ( 'NONE', #205, 4.872650870659752442 ) ;
#5897=( GEOMETRIC_REPRESENTATION_CONTEXT ( 3 ) GLOBAL_UNCERTAINTY_ASSIGNED_CONTEXT ( ( #4802 ) ) GLOBAL_UNIT_ASSIGNED_CONTEXT ( ( #11254, #5679, #5386 ) ) REPRESENTATION_CONTEXT ( 'NONE', 'WORKASPACE' ) );
#5900=DIRECTION ( 'NONE',  ( 1.000000000000000000, 0.000000000000000000, 0.000000000000000000 ) ) ;
#5913=ORIENTED_EDGE ( 'NONE', *, *, #13110, .F. ) ;
#5932=DIRECTION ( 'NONE',  ( 0.1305261922200521840, 0.9914448613738103822, -0.000000000000000000 ) ) ;
#5953=CARTESIAN_POINT ( 'NONE',  ( 0.1374368770859597522, -4.808326913195983821, -0.8000000000000000444 ) ) ;
#5956=ORIENTED_EDGE ( 'NONE', *, *, #16411, .F. ) ;
#6007=DIRECTION ( 'NONE',  ( 1.000000000000000000, 0.000000000000000000, 0.000000000000000000 ) ) ;
#6044=EDGE_LOOP ( 'NONE', ( #13587, #245, #1737, #252 ) ) ;
#6061=CARTESIAN_POINT ( 'NONE',  ( 2.321707774797442170, -4.824281976789052351, -0.8000000000000000444 ) ) ;
#6100=CARTESIAN_POINT ( 'NONE',  ( 4.747884751462026820, -5.143694235355983579, 0.000000000000000000 ) ) ;
#6102=DIRECTION ( 'NONE',  ( 1.000000000000000000, 0.000000000000000000, 0.000000000000000000 ) ) ;
#6135=VERTEX_POINT ( 'NONE', #13718 ) ;
#6141=VERTEX_POINT ( 'NONE', #3434 ) ;
#6148=DIRECTION ( 'NONE',  ( 0.000000000000000000, 0.000000000000000000, 1.000000000000000000 ) ) ;
#6153=ORIENTED_EDGE ( 'NONE', *, *, #1853, .F. ) ;
#6175=AXIS2_PLACEMENT_3D ( 'NONE', #6100, #1691, #10403 ) ;
#6228=ORIENTED_EDGE ( 'NONE', *, *, #16237, .T. ) ;
#6244=VECTOR ( 'NONE', #6704, 1000.000000000000000 ) ;
#6261=EDGE_CURVE ( 'NONE', #6141, #5579, #3168, .T. ) ;
#6267=DIRECTION ( 'NONE',  ( -1.000000000000000000, -0.000000000000000000, -0.000000000000000000 ) ) ;
#6315=DIRECTION ( 'NONE',  ( 1.000000000000000000, 0.000000000000000000, 0.000000000000000000 ) ) ;
#6360=CARTESIAN_POINT ( 'NONE',  ( 0.9999999999999997780, -6.008326913195983998, -0.8000000000000000444 ) ) ;
#6371=AXIS2_PLACEMENT_3D ( 'NONE', #16039, #13083, #1329 ) ;
#6387=ORIENTED_EDGE ( 'NONE', *, *, #5694, .F. ) ;
#6398=CARTESIAN_POINT ( 'NONE',  ( 0.000000000000000000, 0.4273491293402468805, -0.8000000000000000444 ) ) ;
#6427=CARTESIAN_POINT ( 'NONE',  ( 0.000000000000000000, 0.4273491293402468805, -0.8000000000000000444 ) ) ;
#6477=FACE_OUTER_BOUND ( 'NONE', #1218, .T. ) ;
#6480=VERTEX_POINT ( 'NONE', #4694 ) ;
#6488=CYLINDRICAL_SURFACE ( 'NONE', #9515, 4.872650870659752442 ) ;
#6498=VECTOR ( 'NONE', #1295, 1000.000000000000000 ) ;
#6522=DIRECTION ( 'NONE',  ( 0.9995917534020515305, -0.02857142857142857054, 0.000000000000000000 ) ) ;
#6539=DIRECTION ( 'NONE',  ( 0.000000000000000000, 0.000000000000000000, 1.000000000000000000 ) ) ;
#6556=CIRCLE ( 'NONE', #6862, 7.000000000000000000 ) ;
#6592=DIRECTION ( 'NONE',  ( 0.000000000000000000, 0.000000000000000000, 1.000000000000000000 ) ) ;
#6596=CARTESIAN_POINT ( 'NONE',  ( 1.000000000000000000, -4.808326913195983821, -0.8000000000000000444 ) ) ;
#6604=ADVANCED_BREP_SHAPE_REPRESENTATION ( '', ( #14915, #10359 ), #12491 ) ;
#6614=ORIENTED_EDGE ( 'NONE', *, *, #1606, .F. ) ;
#6624=LINE ( 'NONE', #14257, #10561 ) ;
#6638=ORIENTED_EDGE ( 'NONE', *, *, #10234, .T. ) ;
#6700=EDGE_LOOP ( 'NONE', ( #16148, #12706, #18939, #5183 ) ) ;
#6704=DIRECTION ( 'NONE',  ( 1.000000000000000000, -0.000000000000000000, -0.000000000000000000 ) ) ;
#6724=VERTEX_POINT ( 'NONE', #3889 ) ;
#6730=ORIENTED_EDGE ( 'NONE', *, *, #5075, .T. ) ;
#6752=ORIENTED_EDGE ( 'NONE', *, *, #1197, .F. ) ;
#6757=AXIS2_PLACEMENT_3D ( 'NONE', #17436, #17725, #12817 ) ;
#6768=DIRECTION ( 'NONE',  ( 1.000000000000000000, 0.000000000000000000, 0.000000000000000000 ) ) ;
#6774=( NAMED_UNIT ( * ) PLANE_ANGLE_UNIT ( ) SI_UNIT ( $, .RADIAN. ) );
#6783=EDGE_LOOP ( 'NONE', ( #6752, #4722, #6992, #14669 ) ) ;
#6815=PLANE ( 'NONE',  #4306 ) ;
#6833=LINE ( 'NONE', #4890, #17589 ) ;
#6862=AXIS2_PLACEMENT_3D ( 'NONE', #13359, #19381, #17893 ) ;
#6867=VERTEX_POINT ( 'NONE', #18007 ) ;
#6874=DIRECTION ( 'NONE',  ( 0.000000000000000000, 0.000000000000000000, 1.000000000000000000 ) ) ;
#6890=CARTESIAN_POINT ( 'NONE',  ( -1.000000000000000000, -5.408326913195983465, -0.8000000000000000444 ) ) ;
#6911=DIRECTION ( 'NONE',  ( -0.000000000000000000, -0.000000000000000000, -1.000000000000000000 ) ) ;
#6961=DIRECTION ( 'NONE',  ( 0.000000000000000000, 0.000000000000000000, 1.000000000000000000 ) ) ;
#6972=CARTESIAN_POINT ( 'NONE',  ( 0.9999999999999997780, -6.008326913195983998, -0.8000000000000000444 ) ) ;
#6992=ORIENTED_EDGE ( 'NONE', *, *, #7411, .F. ) ;
#7015=DIRECTION ( 'NONE',  ( 0.000000000000000000, 0.000000000000000000, 1.000000000000000000 ) ) ;
#7018=FACE_OUTER_BOUND ( 'NONE', #9194, .T. ) ;
#7030=VERTEX_POINT ( 'NONE', #148 ) ;
#7060=CARTESIAN_POINT ( 'NONE',  ( -1.000000000000000222, -4.808326913195983821, -0.8000000000000000444 ) ) ;
#7069=VECTOR ( 'NONE', #16857, 1000.000000000000000 ) ;
#7073=AXIS2_PLACEMENT_3D ( 'NONE', #10478, #14995, #1678 ) ;
#7093=EDGE_CURVE ( 'NONE', #11712, #11651, #8168, .T. ) ;
#7121=LINE ( 'NONE', #3898, #10900 ) ;
#7126=ADVANCED_FACE ( 'NONE', ( #724 ), #18680, .F. ) ;
#7142=AXIS2_PLACEMENT_3D ( 'NONE', #13333, #13629, #19352 ) ;
#7151=VERTEX_POINT ( 'NONE', #11101 ) ;
#7152=EDGE_LOOP ( 'NONE', ( #5751, #18300, #14175, #4456 ) ) ;
#7209=AXIS2_PLACEMENT_3D ( 'NONE', #8691, #14663, #2442 ) ;
#7216=VERTEX_POINT ( 'NONE', #821 ) ;
#7269=SHAPE_DEFINITION_REPRESENTATION ( #8507, #13919 ) ;
#7293=EDGE_LOOP ( 'NONE', ( #6153, #9734, #7954, #14781 ) ) ;
#7304=CARTESIAN_POINT ( 'NONE',  ( 0.1374368770859596967, -4.808326913195983821, -0.8000000000000000444 ) ) ;
#7323=ORIENTED_EDGE ( 'NONE', *, *, #11157, .T. ) ;
#7333=VERTEX_POINT ( 'NONE', #16023 ) ;
#7338=LINE ( 'NONE', #11740, #14656 ) ;
#7339=ORIENTED_EDGE ( 'NONE', *, *, #8476, .F. ) ;
#7351=FACE_OUTER_BOUND ( 'NONE', #11105, .T. ) ;
#7361=ORIENTED_EDGE ( 'NONE', *, *, #14676, .T. ) ;
#7371=DIRECTION ( 'NONE',  ( 0.000000000000000000, 0.000000000000000000, 1.000000000000000000 ) ) ;
#7374=CARTESIAN_POINT ( 'NONE',  ( 3.160591952521659032, -3.281206521718069258, 0.000000000000000000 ) ) ;
#7376=FACE_OUTER_BOUND ( 'NONE', #10375, .T. ) ;
#7382=DIRECTION ( 'NONE',  ( 0.000000000000000000, 0.000000000000000000, 1.000000000000000000 ) ) ;
#7390=ORIENTED_EDGE ( 'NONE', *, *, #14048, .T. ) ;
#7411=EDGE_CURVE ( 'NONE', #7030, #8472, #13753, .T. ) ;
#7436=VECTOR ( 'NONE', #12834, 1000.000000000000000 ) ;
#7441=CARTESIAN_POINT ( 'NONE',  ( 0.000000000000000000, 0.000000000000000000, -0.8000000000000000444 ) ) ;
#7525=EDGE_CURVE ( 'NONE', #7216, #15143, #14842, .T. ) ;
#7537=DIRECTION ( 'NONE',  ( -0.000000000000000000, -0.000000000000000000, -1.000000000000000000 ) ) ;
#7552=AXIS2_PLACEMENT_3D ( 'NONE', #436, #10812, #13943 ) ;
#7607=LINE ( 'NONE', #16249, #13156 ) ;
#7669=( NAMED_UNIT ( * ) SI_UNIT ( $, .STERADIAN. ) SOLID_ANGLE_UNIT ( ) );
#7696=EDGE_CURVE ( 'NONE', #13512, #6867, #2092, .T. ) ;
#7717=DIRECTION ( 'NONE',  ( 0.000000000000000000, 0.000000000000000000, 1.000000000000000000 ) ) ;
#7731=UNCERTAINTY_MEASURE_WITH_UNIT (LENGTH_MEASURE( 1.000000000000000082E-05 ), #13743, 'distance_accuracy_value', 'NONE');
#7753=AXIS2_PLACEMENT_3D ( 'NONE', #18564, #5106, #11075 ) ;
#7790=CIRCLE ( 'NONE', #14031, 0.7500000000000002220 ) ;
#7795=ORIENTED_EDGE ( 'NONE', *, *, #12431, .T. ) ;
#7823=VERTEX_POINT ( 'NONE', #1468 ) ;
#7832=EDGE_CURVE ( 'NONE', #3492, #18521, #16476, .T. ) ;
#7849=CARTESIAN_POINT ( 'NONE',  ( -0.1085714285714285687, -3.798448662927795372, 0.000000000000000000 ) ) ;
#7863=DIRECTION ( 'NONE',  ( 0.000000000000000000, 0.000000000000000000, 1.000000000000000000 ) ) ;
#7865=( LENGTH_UNIT ( ) NAMED_UNIT ( * ) SI_UNIT ( .MILLI., .METRE. ) );
#7882=EDGE_CURVE ( 'NONE', #17851, #12908, #12334, .T. ) ;
#7896=DIRECTION ( 'NONE',  ( 0.9995917534020515305, -0.02857142857142857054, 0.000000000000000000 ) ) ;
#7954=ORIENTED_EDGE ( 'NONE', *, *, #12189, .T. ) ;
#7979=AXIS2_PLACEMENT_3D ( 'NONE', #17171, #2668, #11556 ) ;
#7981=DIRECTION ( 'NONE',  ( 0.02857142857142857054, -0.9995917534020515305, 0.000000000000000000 ) ) ;
#8007=CARTESIAN_POINT ( 'NONE',  ( -3.799999999999999378, 4.653657836759941744E-16, -0.8000000000000000444 ) ) ;
#8022=CARTESIAN_POINT ( 'NONE',  ( -3.160591952521660364, -3.281206521718067037, -0.8000000000000000444 ) ) ;
#8063=CIRCLE ( 'NONE', #8375, 0.5999999999999998668 ) ;
#8074=ORIENTED_EDGE ( 'NONE', *, *, #2152, .T. ) ;
#8079=ORIENTED_EDGE ( 'NONE', *, *, #18997, .T. ) ;
#8143=AXIS2_PLACEMENT_3D ( 'NONE', #17205, #15725, #14237 ) ;
#8146=( NAMED_UNIT ( * ) SI_UNIT ( $, .STERADIAN. ) SOLID_ANGLE_UNIT ( ) );
#8168=CIRCLE ( 'NONE', #7552, 0.5999999999999998668 ) ;
#8182=EDGE_LOOP ( 'NONE', ( #5228, #18965, #6228, #19328 ) ) ;
#8238=DIRECTION ( 'NONE',  ( 1.000000000000000000, 0.000000000000000000, 0.000000000000000000 ) ) ;
#8261=ORIENTED_EDGE ( 'NONE', *, *, #2195, .F. ) ;
#8311=ORIENTED_EDGE ( 'NONE', *, *, #772, .F. ) ;
#8342=CIRCLE ( 'NONE', #12115, 2.447112362156698140 ) ;
#8375=AXIS2_PLACEMENT_3D ( 'NONE', #12851, #17669, #8238 ) ;
#8403=CARTESIAN_POINT ( 'NONE',  ( 0.1085714285714285687, -3.798448662927795372, -0.8000000000000000444 ) ) ;
#8408=VERTEX_POINT ( 'NONE', #13595 ) ;
#8449=EDGE_CURVE ( 'NONE', #15433, #16449, #6624, .T. ) ;
#8471=CIRCLE ( 'NONE', #10338, 4.872650870659752442 ) ;
#8472=VERTEX_POINT ( 'NONE', #11029 ) ;
#8476=EDGE_CURVE ( 'NONE', #14776, #7333, #860, .T. ) ;
#8477=DIRECTION ( 'NONE',  ( 0.000000000000000000, 0.000000000000000000, 1.000000000000000000 ) ) ;
#8507=PRODUCT_DEFINITION_SHAPE ( 'NONE', 'NONE',  #13215 ) ;
#8517=DIRECTION ( 'NONE',  ( 0.1305261922200521840, -0.9914448613738103822, 0.000000000000000000 ) ) ;
#8524=CARTESIAN_POINT ( 'NONE',  ( 4.872650870659752442, 0.4273491293402468805, -0.8000000000000000444 ) ) ;
#8548=ADVANCED_FACE ( 'NONE', ( #16936 ), #6815, .T. ) ;
#8604=PLANE ( 'NONE',  #15820 ) ;
#8660=ORIENTED_EDGE ( 'NONE', *, *, #9258, .T. ) ;
#8691=CARTESIAN_POINT ( 'NONE',  ( 1.000000000000000000, -5.408326913195983465, 0.000000000000000000 ) ) ;
#8702=DIRECTION ( 'NONE',  ( 0.02857142857142857401, 0.9995917534020515305, -0.000000000000000000 ) ) ;
#8725=PLANE ( 'NONE',  #16025 ) ;
#8758=VERTEX_POINT ( 'NONE', #19398 ) ;
#8769=APPLICATION_CONTEXT ( 'automotive_design' ) ;
#8785=ORIENTED_EDGE ( 'NONE', *, *, #16169, .T. ) ;
#8834=DIRECTION ( 'NONE',  ( 0.000000000000000000, 0.000000000000000000, 1.000000000000000000 ) ) ;
#8844=CARTESIAN_POINT ( 'NONE',  ( -1.566204647097437563, -6.822536405429463713, -0.8000000000000000444 ) ) ;
#8847=CARTESIAN_POINT ( 'NONE',  ( -3.160591952521660364, -3.281206521718067037, -0.8000000000000000444 ) ) ;
#8862=FACE_OUTER_BOUND ( 'NONE', #8993, .T. ) ;
#8912=AXIS2_PLACEMENT_3D ( 'NONE', #6360, #4806, #4985 ) ;
#8944=VERTEX_POINT ( 'NONE', #14658 ) ;
#8955=CARTESIAN_POINT ( 'NONE',  ( -0.2000000000000000111, -6.997142273814360713, -0.8000000000000000444 ) ) ;
#8957=EDGE_CURVE ( 'NONE', #15433, #11712, #1725, .T. ) ;
#8978=ORIENTED_EDGE ( 'NONE', *, *, #7832, .T. ) ;
#8993=EDGE_LOOP ( 'NONE', ( #10563, #14878, #17894, #2091 ) ) ;
#9019=CARTESIAN_POINT ( 'NONE',  ( 0.000000000000000000, 0.000000000000000000, 0.000000000000000000 ) ) ;
#9065=ORIENTED_EDGE ( 'NONE', *, *, #1976, .F. ) ;
#9068=AXIS2_PLACEMENT_3D ( 'NONE', #2778, #7371, #19065 ) ;
#9081=DIRECTION ( 'NONE',  ( 0.000000000000000000, 0.000000000000000000, -1.000000000000000000 ) ) ;
#9092=VERTEX_POINT ( 'NONE', #900 ) ;
#9122=FACE_OUTER_BOUND ( 'NONE', #9740, .T. ) ;
#9154=DIRECTION ( 'NONE',  ( 0.000000000000000000, 0.000000000000000000, 1.000000000000000000 ) ) ;
#9157=DIRECTION ( 'NONE',  ( 0.000000000000000000, 0.000000000000000000, 1.000000000000000000 ) ) ;
#9172=EDGE_CURVE ( 'NONE', #17851, #8408, #14421, .T. ) ;
#9194=EDGE_LOOP ( 'NONE', ( #10264, #14096, #13904, #9259 ) ) ;
#9199=CARTESIAN_POINT ( 'NONE',  ( -1.000000000000000000, -6.008326913195983998, -0.8000000000000000444 ) ) ;
#9228=( NAMED_UNIT ( * ) PLANE_ANGLE_UNIT ( ) SI_UNIT ( $, .RADIAN. ) );
#9233=EDGE_CURVE ( 'NONE', #10636, #6141, #5488, .T. ) ;
#9236=ORIENTED_EDGE ( 'NONE', *, *, #13243, .F. ) ;
#9249=EDGE_CURVE ( 'NONE', #6480, #8472, #794, .T. ) ;
#9255=FACE_OUTER_BOUND ( 'NONE', #8182, .T. ) ;
#9258=EDGE_CURVE ( 'NONE', #3492, #1565, #16590, .T. ) ;
#9259=ORIENTED_EDGE ( 'NONE', *, *, #5677, .T. ) ;
#9267=AXIS2_PLACEMENT_3D ( 'NONE', #11852, #4421, #10183 ) ;
#9295=CIRCLE ( 'NONE', #6175, 2.447112362156698140 ) ;
#9319=DIRECTION ( 'NONE',  ( 0.000000000000000000, 0.000000000000000000, 1.000000000000000000 ) ) ;
#9326=SURFACE_SIDE_STYLE ('',( #10794 ) ) ;
#9372=ADVANCED_FACE ( 'NONE', ( #4817 ), #3255, .T. ) ;
#9377=LINE ( 'NONE', #8007, #7069 ) ;
#9427=AXIS2_PLACEMENT_3D ( 'NONE', #4032, #4129, #6768 ) ;
#9454=ORIENTED_EDGE ( 'NONE', *, *, #1734, .F. ) ;
#9515=AXIS2_PLACEMENT_3D ( 'NONE', #6398, #6592, #9720 ) ;
#9538=DIRECTION ( 'NONE',  ( 0.000000000000000000, 0.000000000000000000, 1.000000000000000000 ) ) ;
#9571=AXIS2_PLACEMENT_3D ( 'NONE', #993, #6961, #12940 ) ;
#9579=DIRECTION ( 'NONE',  ( 1.000000000000000000, 0.000000000000000000, 0.000000000000000000 ) ) ;
#9584=LINE ( 'NONE', #15390, #18740 ) ;
#9593=FACE_OUTER_BOUND ( 'NONE', #6044, .T. ) ;
#9705=CARTESIAN_POINT ( 'NONE',  ( -2.321707774797442170, -4.824281976789052351, 0.000000000000000000 ) ) ;
#9711=LINE ( 'NONE', #3746, #13142 ) ;
#9720=DIRECTION ( 'NONE',  ( 1.000000000000000000, 0.000000000000000000, 0.000000000000000000 ) ) ;
#9734=ORIENTED_EDGE ( 'NONE', *, *, #16598, .F. ) ;
#9740=EDGE_LOOP ( 'NONE', ( #18838, #12466, #16635, #15962 ) ) ;
#9782=CARTESIAN_POINT ( 'NONE',  ( -4.872650870659752442, 0.4273491293402474911, 0.000000000000000000 ) ) ;
#9826=ORIENTED_EDGE ( 'NONE', *, *, #7525, .T. ) ;
#9827=LINE ( 'NONE', #11307, #13749 ) ;
#9854=EDGE_CURVE ( 'NONE', #2618, #7151, #3014, .T. ) ;
#9904=EDGE_CURVE ( 'NONE', #2618, #6141, #9377, .T. ) ;
#9954=CARTESIAN_POINT ( 'NONE',  ( -1.000000000000000222, -4.808326913195983821, -0.8000000000000000444 ) ) ;
#9955=ORIENTED_EDGE ( 'NONE', *, *, #7093, .F. ) ;
#9967=LINE ( 'NONE', #15969, #17095 ) ;
#9989=DIRECTION ( 'NONE',  ( 0.1305261922200521840, -0.9914448613738103822, 0.000000000000000000 ) ) ;
#10006=CARTESIAN_POINT ( 'NONE',  ( -3.160591952521660364, -3.281206521718067037, 0.000000000000000000 ) ) ;
#10011=ORIENTED_EDGE ( 'NONE', *, *, #16598, .T. ) ;
#10029=ORIENTED_EDGE ( 'NONE', *, *, #10347, .F. ) ;
#10054=CARTESIAN_POINT ( 'NONE',  ( 2.321707774797442170, -4.824281976789052351, 0.000000000000000000 ) ) ;
#10056=ORIENTED_EDGE ( 'NONE', *, *, #2015, .T. ) ;
#10058=DIRECTION ( 'NONE',  ( -0.000000000000000000, 1.000000000000000000, 0.000000000000000000 ) ) ;
#10060=AXIS2_PLACEMENT_3D ( 'NONE', #12654, #18463, #13833 ) ;
#10100=EDGE_CURVE ( 'NONE', #18734, #12908, #10809, .T. ) ;
#10183=DIRECTION ( 'NONE',  ( 1.000000000000000000, 0.000000000000000000, 0.000000000000000000 ) ) ;
#10193=DIRECTION ( 'NONE',  ( 1.000000000000000000, -0.000000000000000000, -0.000000000000000000 ) ) ;
#10217=CIRCLE ( 'NONE', #15876, 0.7500000000000002220 ) ;
#10228=AXIS2_PLACEMENT_3D ( 'NONE', #17078, #16786, #3449 ) ;
#10234=EDGE_CURVE ( 'NONE', #12595, #15728, #627, .T. ) ;
#10259=FACE_OUTER_BOUND ( 'NONE', #5225, .T. ) ;
#10264=ORIENTED_EDGE ( 'NONE', *, *, #4249, .F. ) ;
#10271=ORIENTED_EDGE ( 'NONE', *, *, #4838, .F. ) ;
#10273=ORIENTED_EDGE ( 'NONE', *, *, #11670, .F. ) ;
#10304=DIRECTION ( 'NONE',  ( 0.02857142857142857054, -0.9995917534020515305, 0.000000000000000000 ) ) ;
#10338=AXIS2_PLACEMENT_3D ( 'NONE', #11879, #7382, #17887 ) ;
#10347=EDGE_CURVE ( 'NONE', #1565, #18734, #7607, .T. ) ;
#10359=AXIS2_PLACEMENT_3D ( 'NONE', #2871, #8834, #16191 ) ;
#10369=ORIENTED_EDGE ( 'NONE', *, *, #635, .T. ) ;
#10372=CIRCLE ( 'NONE', #10060, 4.872650870659752442 ) ;
#10375=EDGE_LOOP ( 'NONE', ( #12524, #14757, #2290, #10434 ) ) ;
#10399=CARTESIAN_POINT ( 'NONE',  ( -1.000000000000000222, -4.808326913195983821, -0.8000000000000000444 ) ) ;
#10403=DIRECTION ( 'NONE',  ( 1.000000000000000000, 0.000000000000000000, 0.000000000000000000 ) ) ;
#10416=VERTEX_POINT ( 'NONE', #12206 ) ;
#10434=ORIENTED_EDGE ( 'NONE', *, *, #3888, .T. ) ;
#10445=ORIENTED_EDGE ( 'NONE', *, *, #3526, .F. ) ;
#10478=CARTESIAN_POINT ( 'NONE',  ( 0.000000000000000000, 0.000000000000000000, -0.8000000000000000444 ) ) ;
#10491=DIRECTION ( 'NONE',  ( 1.000000000000000000, 0.000000000000000000, 0.000000000000000000 ) ) ;
#10561=VECTOR ( 'NONE', #17035, 1000.000000000000000 ) ;
#10563=ORIENTED_EDGE ( 'NONE', *, *, #5576, .T. ) ;
#10593=ADVANCED_FACE ( 'NONE', ( #9255 ), #15245, .T. ) ;
#10596=DIRECTION ( 'NONE',  ( 0.000000000000000000, 0.000000000000000000, 1.000000000000000000 ) ) ;
#10636=VERTEX_POINT ( 'NONE', #11019 ) ;
#10659=VECTOR ( 'NONE', #1762, 1000.000000000000114 ) ;
#10695=DIRECTION ( 'NONE',  ( 0.000000000000000000, 0.000000000000000000, 1.000000000000000000 ) ) ;
#10753=DIRECTION ( 'NONE',  ( 1.000000000000000000, 0.000000000000000000, 0.000000000000000000 ) ) ;
#10761=ORIENTED_EDGE ( 'NONE', *, *, #2088, .T. ) ;
#10777=ORIENTED_EDGE ( 'NONE', *, *, #9854, .T. ) ;
#10780=DIRECTION ( 'NONE',  ( 0.000000000000000000, 0.000000000000000000, 1.000000000000000000 ) ) ;
#10781=CARTESIAN_POINT ( 'NONE',  ( 1.566204647097437341, -6.822536405429464601, -0.8000000000000000444 ) ) ;
#10794=SURFACE_STYLE_FILL_AREA ( #18573 ) ;
#10809=CIRCLE ( 'NONE', #6757, 0.5999999999999999778 ) ;
#10812=DIRECTION ( 'NONE',  ( 0.000000000000000000, 0.000000000000000000, 1.000000000000000000 ) ) ;
#10836=EDGE_CURVE ( 'NONE', #18521, #18734, #19285, .T. ) ;
#10893=DIRECTION ( 'NONE',  ( -1.000000000000000000, -0.000000000000000000, -0.000000000000000000 ) ) ;
#10900=VECTOR ( 'NONE', #11133, 1000.000000000000114 ) ;
#10912=ORIENTED_EDGE ( 'NONE', *, *, #7093, .T. ) ;
#10918=CARTESIAN_POINT ( 'NONE',  ( 1.599999999999999867, -5.408326913195983465, 0.000000000000000000 ) ) ;
#10933=VECTOR ( 'NONE', #12255, 1000.000000000000000 ) ;
#10970=CARTESIAN_POINT ( 'NONE',  ( 2.321707774797442170, -4.824281976789052351, -0.8000000000000000444 ) ) ;
#11019=CARTESIAN_POINT ( 'NONE',  ( -0.1085714285714285687, -3.798448662927795372, 0.000000000000000000 ) ) ;
#11029=CARTESIAN_POINT ( 'NONE',  ( -0.2000000000000000111, -6.997142273814360713, 0.000000000000000000 ) ) ;
#11075=DIRECTION ( 'NONE',  ( 1.000000000000000000, 0.000000000000000000, 0.000000000000000000 ) ) ;
#11101=CARTESIAN_POINT ( 'NONE',  ( 3.799999999999999378, 0.000000000000000000, -0.8000000000000000444 ) ) ;
#11105=EDGE_LOOP ( 'NONE', ( #10912, #4047, #10761, #10271, #12046, #1370, #6387, #15265, #8660, #18108, #16649, #5956, #9065, #18694, #8261, #7339, #1662, #11469, #18940, #6614, #14879, #13271, #9454, #1933, #11256 ) ) ;
#11133=DIRECTION ( 'NONE',  ( 0.02857142857142857401, -0.9995917534020515305, 0.000000000000000000 ) ) ;
#11157=EDGE_CURVE ( 'NONE', #7151, #5579, #6833, .T. ) ;
#11179=ADVANCED_FACE ( 'NONE', ( #5757 ), #19218, .F. ) ;
#11210=MECHANICAL_DESIGN_GEOMETRIC_PRESENTATION_REPRESENTATION('',(#1840),#5897);
#11233=( GEOMETRIC_REPRESENTATION_CONTEXT ( 3 ) GLOBAL_UNCERTAINTY_ASSIGNED_CONTEXT ( ( #288 ) ) GLOBAL_UNIT_ASSIGNED_CONTEXT ( ( #7865, #6774, #8146 ) ) REPRESENTATION_CONTEXT ( 'NONE', 'WORKASPACE' ) );
#11254=( LENGTH_UNIT ( ) NAMED_UNIT ( * ) SI_UNIT ( .MILLI., .METRE. ) );
#11256=ORIENTED_EDGE ( 'NONE', *, *, #8957, .T. ) ;
#11307=CARTESIAN_POINT ( 'NONE',  ( -0.1085714285714285687, -3.798448662927795372, -0.8000000000000000444 ) ) ;
#11336=ORIENTED_EDGE ( 'NONE', *, *, #7882, .T. ) ;
#11357=ORIENTED_EDGE ( 'NONE', *, *, #1914, .T. ) ;
#11364=LINE ( 'NONE', #17468, #2669 ) ;
#11387=CYLINDRICAL_SURFACE ( 'NONE', #12953, 0.5999999999999998668 ) ;
#11425=ORIENTED_EDGE ( 'NONE', *, *, #7696, .T. ) ;
#11431=ORIENTED_EDGE ( 'NONE', *, *, #16591, .T. ) ;
#11433=AXIS2_PLACEMENT_3D ( 'NONE', #210, #10780, #12160 ) ;
#11436=EDGE_LOOP ( 'NONE', ( #11517, #1622, #6730, #8785 ) ) ;
#11469=ORIENTED_EDGE ( 'NONE', *, *, #5576, .F. ) ;
#11479=EDGE_LOOP ( 'NONE', ( #5913, #9955, #12209, #6638 ) ) ;
#11517=ORIENTED_EDGE ( 'NONE', *, *, #772, .T. ) ;
#11534=ADVANCED_FACE ( 'NONE', ( #17121 ), #16929, .T. ) ;
#11556=DIRECTION ( 'NONE',  ( 1.000000000000000000, 0.000000000000000000, 0.000000000000000000 ) ) ;
#11633=ORIENTED_EDGE ( 'NONE', *, *, #17924, .F. ) ;
#11639=DIRECTION ( 'NONE',  ( -0.000000000000000000, -0.000000000000000000, -1.000000000000000000 ) ) ;
#11651=VERTEX_POINT ( 'NONE', #5051 ) ;
#11670=EDGE_CURVE ( 'NONE', #6724, #2159, #935, .T. ) ;
#11709=ORIENTED_EDGE ( 'NONE', *, *, #12568, .T. ) ;
#11712=VERTEX_POINT ( 'NONE', #5526 ) ;
#11718=AXIS2_PLACEMENT_3D ( 'NONE', #17879, #10695, #1307 ) ;
#11723=DIRECTION ( 'NONE',  ( 0.000000000000000000, 0.000000000000000000, 1.000000000000000000 ) ) ;
#11740=CARTESIAN_POINT ( 'NONE',  ( 0.9999999999999997780, -6.008326913195983998, -0.8000000000000000444 ) ) ;
#11817=VECTOR ( 'NONE', #19368, 1000.000000000000000 ) ;
#11840=CARTESIAN_POINT ( 'NONE',  ( 2.321707774797442170, -4.824281976789052351, -0.8000000000000000444 ) ) ;
#11852=CARTESIAN_POINT ( 'NONE',  ( 0.000000000000000000, 0.000000000000000000, -0.8000000000000000444 ) ) ;
#11867=CARTESIAN_POINT ( 'NONE',  ( 1.000000000000000000, -5.408326913195983465, 0.000000000000000000 ) ) ;
#11868=DIRECTION ( 'NONE',  ( 1.000000000000000000, -0.000000000000000000, -0.000000000000000000 ) ) ;
#11879=CARTESIAN_POINT ( 'NONE',  ( 0.000000000000000000, 0.4273491293402468805, 0.000000000000000000 ) ) ;
#11940=CARTESIAN_POINT ( 'NONE',  ( 0.1085714285714285687, -3.798448662927795372, 0.000000000000000000 ) ) ;
#11970=EDGE_CURVE ( 'NONE', #16413, #12819, #8342, .T. ) ;
#11976=LINE ( 'NONE', #8844, #11817 ) ;
#12038=ADVANCED_FACE ( 'NONE', ( #8862 ), #1419, .T. ) ;
#12046=ORIENTED_EDGE ( 'NONE', *, *, #18903, .F. ) ;
#12071=CARTESIAN_POINT ( 'NONE',  ( 4.747884751462026820, -5.143694235355983579, -0.8000000000000000444 ) ) ;
#12072=AXIS2_PLACEMENT_3D ( 'NONE', #1286, #12146, #9579 ) ;
#12090=ORIENTED_EDGE ( 'NONE', *, *, #10836, .F. ) ;
#12109=CLOSED_SHELL ( 'NONE', ( #12794, #12038, #17852, #174, #11179, #11534, #1510, #5188, #8548, #3872, #9372, #13993, #13118, #3532, #1424, #4850, #3203, #18330, #10593, #1956, #18042, #5201, #7126, #5730, #460, #4491, #15286 ) ) ;
#12115=AXIS2_PLACEMENT_3D ( 'NONE', #1326, #16621, #231 ) ;
#12140=LINE ( 'NONE', #18147, #10659 ) ;
#12146=DIRECTION ( 'NONE',  ( 0.000000000000000000, 0.000000000000000000, 1.000000000000000000 ) ) ;
#12159=ORIENTED_EDGE ( 'NONE', *, *, #9172, .F. ) ;
#12160=DIRECTION ( 'NONE',  ( 1.000000000000000000, 0.000000000000000000, 0.000000000000000000 ) ) ;
#12189=EDGE_CURVE ( 'NONE', #9092, #7216, #10217, .T. ) ;
#12198=VECTOR ( 'NONE', #4629, 1000.000000000000114 ) ;
#12200=ORIENTED_EDGE ( 'NONE', *, *, #6261, .F. ) ;
#12206=CARTESIAN_POINT ( 'NONE',  ( 1.000000000000000000, -4.808326913195983821, 0.000000000000000000 ) ) ;
#12209=ORIENTED_EDGE ( 'NONE', *, *, #15140, .T. ) ;
#12226=ORIENTED_EDGE ( 'NONE', *, *, #9249, .T. ) ;
#12246=DIRECTION ( 'NONE',  ( 0.000000000000000000, 0.000000000000000000, 1.000000000000000000 ) ) ;
#12255=DIRECTION ( 'NONE',  ( 0.000000000000000000, 0.000000000000000000, 1.000000000000000000 ) ) ;
#12288=FACE_OUTER_BOUND ( 'NONE', #3292, .T. ) ;
#12300=EDGE_LOOP ( 'NONE', ( #19302, #246, #13651, #18211 ) ) ;
#12334=LINE ( 'NONE', #9199, #3061 ) ;
#12364=VECTOR ( 'NONE', #8702, 1000.000000000000114 ) ;
#12402=APPLICATION_CONTEXT ( 'automotive_design' ) ;
#12412=VECTOR ( 'NONE', #9154, 1000.000000000000000 ) ;
#12431=EDGE_CURVE ( 'NONE', #15728, #10416, #15891, .T. ) ;
#12464=CYLINDRICAL_SURFACE ( 'NONE', #13457, 4.872650870659752442 ) ;
#12466=ORIENTED_EDGE ( 'NONE', *, *, #5446, .F. ) ;
#12491=( GEOMETRIC_REPRESENTATION_CONTEXT ( 3 ) GLOBAL_UNCERTAINTY_ASSIGNED_CONTEXT ( ( #7731 ) ) GLOBAL_UNIT_ASSIGNED_CONTEXT ( ( #13743, #9228, #7669 ) ) REPRESENTATION_CONTEXT ( 'NONE', 'WORKASPACE' ) );
#12510=ORIENTED_EDGE ( 'NONE', *, *, #9233, .T. ) ;
#12524=ORIENTED_EDGE ( 'NONE', *, *, #58, .F. ) ;
#12557=CARTESIAN_POINT ( 'NONE',  ( -1.566204647097437563, -6.822536405429463713, -0.8000000000000000444 ) ) ;
#12559=CARTESIAN_POINT ( 'NONE',  ( -2.141980652367355020, -6.189445006155633422, -0.8000000000000000444 ) ) ;
#12568=EDGE_CURVE ( 'NONE', #2066, #14471, #2566, .T. ) ;
#12571=CARTESIAN_POINT ( 'NONE',  ( -1.000000000000000000, -6.008326913195983998, -0.8000000000000000444 ) ) ;
#12575=CARTESIAN_POINT ( 'NONE',  ( 0.000000000000000000, 0.000000000000000000, 0.000000000000000000 ) ) ;
#12577=DIRECTION ( 'NONE',  ( 0.000000000000000000, 0.000000000000000000, -1.000000000000000000 ) ) ;
#12579=FACE_OUTER_BOUND ( 'NONE', #16662, .T. ) ;
#12593=ORIENTED_EDGE ( 'NONE', *, *, #18903, .T. ) ;
#12595=VERTEX_POINT ( 'NONE', #17359 ) ;
#12639=ORIENTED_EDGE ( 'NONE', *, *, #3888, .F. ) ;
#12654=CARTESIAN_POINT ( 'NONE',  ( 0.000000000000000000, 0.4273491293402468805, -0.8000000000000000444 ) ) ;
#12661=ORIENTED_EDGE ( 'NONE', *, *, #58, .T. ) ;
#12668=VERTEX_POINT ( 'NONE', #419 ) ;
#12675=CYLINDRICAL_SURFACE ( 'NONE', #2956, 3.799999999999999378 ) ;
#12706=ORIENTED_EDGE ( 'NONE', *, *, #1416, .F. ) ;
#12708=DIRECTION ( 'NONE',  ( 0.1305261922200521840, -0.9914448613738103822, 0.000000000000000000 ) ) ;
#12765=DIRECTION ( 'NONE',  ( 0.000000000000000000, 0.000000000000000000, 1.000000000000000000 ) ) ;
#12794=ADVANCED_FACE ( 'NONE', ( #6477 ), #15314, .F. ) ;
#12802=DIRECTION ( 'NONE',  ( 0.02857142857142857054, 0.9995917534020515305, 0.000000000000000000 ) ) ;
#12817=DIRECTION ( 'NONE',  ( 1.000000000000000000, 0.000000000000000000, 0.000000000000000000 ) ) ;
#12819=VERTEX_POINT ( 'NONE', #9705 ) ;
#12834=DIRECTION ( 'NONE',  ( 0.000000000000000000, 0.000000000000000000, 1.000000000000000000 ) ) ;
#12851=CARTESIAN_POINT ( 'NONE',  ( 1.000000000000000000, -5.408326913195983465, -0.8000000000000000444 ) ) ;
#12865=DIRECTION ( 'NONE',  ( 1.000000000000000000, 0.000000000000000000, 0.000000000000000000 ) ) ;
#12900=DIRECTION ( 'NONE',  ( 1.000000000000000000, 0.000000000000000000, 0.000000000000000000 ) ) ;
#12908=VERTEX_POINT ( 'NONE', #19053 ) ;
#12940=DIRECTION ( 'NONE',  ( -1.000000000000000000, 0.000000000000000000, 0.000000000000000000 ) ) ;
#12953=AXIS2_PLACEMENT_3D ( 'NONE', #14620, #1206, #18970 ) ;
#12958=EDGE_CURVE ( 'NONE', #11651, #488, #8063, .T. ) ;
#13000=CARTESIAN_POINT ( 'NONE',  ( -2.321707774797442170, -4.824281976789052351, -0.8000000000000000444 ) ) ;
#13083=DIRECTION ( 'NONE',  ( 0.000000000000000000, 0.000000000000000000, 1.000000000000000000 ) ) ;
#13086=LINE ( 'NONE', #7304, #15110 ) ;
#13110=EDGE_CURVE ( 'NONE', #11651, #15728, #4324, .T. ) ;
#13118=ADVANCED_FACE ( 'NONE', ( #9122 ), #1385, .F. ) ;
#13142=VECTOR ( 'NONE', #15712, 1000.000000000000000 ) ;
#13156=VECTOR ( 'NONE', #72, 1000.000000000000000 ) ;
#13211=CARTESIAN_POINT ( 'NONE',  ( -0.1085714285714285687, -3.798448662927795372, 0.000000000000000000 ) ) ;
#13215=PRODUCT_DEFINITION ( 'UNKNOWN', '', #15757, #2050 ) ;
#13225=VECTOR ( 'NONE', #17013, 1000.000000000000000 ) ;
#13243=EDGE_CURVE ( 'NONE', #3598, #13512, #9584, .T. ) ;
#13252=LINE ( 'NONE', #16309, #1395 ) ;
#13271=ORIENTED_EDGE ( 'NONE', *, *, #12189, .F. ) ;
#13300=VECTOR ( 'NONE', #15150, 1000.000000000000000 ) ;
#13333=CARTESIAN_POINT ( 'NONE',  ( -4.747884751462026820, -5.143694235355983579, -0.8000000000000000444 ) ) ;
#13359=CARTESIAN_POINT ( 'NONE',  ( 0.000000000000000000, 0.000000000000000000, 0.000000000000000000 ) ) ;
#13371=CARTESIAN_POINT ( 'NONE',  ( 2.321707774797442170, -4.824281976789052351, -0.8000000000000000444 ) ) ;
#13450=PLANE ( 'NONE',  #4007 ) ;
#13452=LINE ( 'NONE', #8847, #3197 ) ;
#13457=AXIS2_PLACEMENT_3D ( 'NONE', #2492, #12765, #18764 ) ;
#13512=VERTEX_POINT ( 'NONE', #11940 ) ;
#13587=ORIENTED_EDGE ( 'NONE', *, *, #5694, .T. ) ;
#13595=CARTESIAN_POINT ( 'NONE',  ( -0.1717365941144614327, -6.008326913195983998, -0.8000000000000000444 ) ) ;
#13629=DIRECTION ( 'NONE',  ( 0.000000000000000000, 0.000000000000000000, 1.000000000000000000 ) ) ;
#13632=VERTEX_POINT ( 'NONE', #5770 ) ;
#13651=ORIENTED_EDGE ( 'NONE', *, *, #13710, .T. ) ;
#13678=ORIENTED_EDGE ( 'NONE', *, *, #5446, .T. ) ;
#13710=EDGE_CURVE ( 'NONE', #6135, #1616, #7790, .T. ) ;
#13718=CARTESIAN_POINT ( 'NONE',  ( -2.141980652367355020, -6.189445006155633422, -0.8000000000000000444 ) ) ;
#13743=( LENGTH_UNIT ( ) NAMED_UNIT ( * ) SI_UNIT ( .MILLI., .METRE. ) );
#13749=VECTOR ( 'NONE', #9538, 1000.000000000000000 ) ;
#13751=DIRECTION ( 'NONE',  ( 1.000000000000000000, 0.000000000000000000, 0.000000000000000000 ) ) ;
#13753=LINE ( 'NONE', #8955, #12412 ) ;
#13757=CARTESIAN_POINT ( 'NONE',  ( -2.321707774797442170, -4.824281976789052351, -0.8000000000000000444 ) ) ;
#13833=DIRECTION ( 'NONE',  ( 1.000000000000000000, 0.000000000000000000, 0.000000000000000000 ) ) ;
#13838=DIRECTION ( 'NONE',  ( 1.000000000000000000, 0.000000000000000000, 0.000000000000000000 ) ) ;
#13904=ORIENTED_EDGE ( 'NONE', *, *, #2195, .T. ) ;
#13919=SHAPE_REPRESENTATION ( 'circlip for shafts normal_din_Circlip DIN 471 - 8 x 0.8', ( #10359 ), #12491 ) ;
#13941=AXIS2_PLACEMENT_3D ( 'NONE', #7441, #7537, #1756 ) ;
#13943=DIRECTION ( 'NONE',  ( 1.000000000000000000, 0.000000000000000000, 0.000000000000000000 ) ) ;
#13949=EDGE_LOOP ( 'NONE', ( #10056, #11709, #5279, #12639 ) ) ;
#13954=DIRECTION ( 'NONE',  ( -0.9995917534020515305, -0.02857142857142857054, 0.000000000000000000 ) ) ;
#13989=DIRECTION ( 'NONE',  ( 1.000000000000000000, 0.000000000000000000, 0.000000000000000000 ) ) ;
#13993=ADVANCED_FACE ( 'NONE', ( #7018 ), #5359, .T. ) ;
#14013=CARTESIAN_POINT ( 'NONE',  ( 2.141980652367355464, -6.189445006155633422, 0.000000000000000000 ) ) ;
#14020=PRODUCT_CONTEXT ( 'NONE', #8769, 'mechanical' ) ;
#14031=AXIS2_PLACEMENT_3D ( 'NONE', #379, #7717, #10753 ) ;
#14041=ORIENTED_EDGE ( 'NONE', *, *, #1734, .T. ) ;
#14048=EDGE_CURVE ( 'NONE', #5656, #17997, #14169, .T. ) ;
#14055=STYLED_ITEM ( 'NONE', ( #1895 ), #6604 ) ;
#14070=ORIENTED_EDGE ( 'NONE', *, *, #10100, .T. ) ;
#14082=VECTOR ( 'NONE', #9319, 1000.000000000000000 ) ;
#14096=ORIENTED_EDGE ( 'NONE', *, *, #893, .F. ) ;
#14147=LINE ( 'NONE', #731, #6244 ) ;
#14169=LINE ( 'NONE', #10054, #15300 ) ;
#14175=ORIENTED_EDGE ( 'NONE', *, *, #14423, .T. ) ;
#14228=LINE ( 'NONE', #4932, #5568 ) ;
#14230=AXIS2_PLACEMENT_3D ( 'NONE', #4780, #170, #9081 ) ;
#14237=DIRECTION ( 'NONE',  ( 1.000000000000000000, 0.000000000000000000, 0.000000000000000000 ) ) ;
#14238=AXIS2_PLACEMENT_3D ( 'NONE', #9019, #15009, #6007 ) ;
#14257=CARTESIAN_POINT ( 'NONE',  ( 0.1717365941144614605, -6.008326913195983998, -0.8000000000000000444 ) ) ;
#14273=PRODUCT ( 'circlip for shafts normal_din_Circlip DIN 471 - 8 x 0.8', 'circlip for shafts normal_din_Circlip DIN 471 - 8 x 0.8', '', ( #14020 ) ) ;
#14274=CIRCLE ( 'NONE', #9571, 0.7500000000000002220 ) ;
#14311=DIRECTION ( 'NONE',  ( -0.000000000000000000, 1.000000000000000000, 0.000000000000000000 ) ) ;
#14376=CARTESIAN_POINT ( 'NONE',  ( 0.000000000000000000, 0.000000000000000000, -0.8000000000000000444 ) ) ;
#14421=LINE ( 'NONE', #6972, #4871 ) ;
#14423=EDGE_CURVE ( 'NONE', #8944, #10636, #9827, .T. ) ;
#14429=FACE_OUTER_BOUND ( 'NONE', #13949, .T. ) ;
#14444=AXIS2_PLACEMENT_3D ( 'NONE', #3493, #7896, #15640 ) ;
#14456=CARTESIAN_POINT ( 'NONE',  ( -4.872650870659752442, 0.4273491293402474911, -0.8000000000000000444 ) ) ;
#14471=VERTEX_POINT ( 'NONE', #18785 ) ;
#14566=AXIS2_PLACEMENT_3D ( 'NONE', #115, #17974, #10491 ) ;
#14586=CIRCLE ( 'NONE', #9267, 7.000000000000000000 ) ;
#14594=FACE_OUTER_BOUND ( 'NONE', #2106, .T. ) ;
#14620=CARTESIAN_POINT ( 'NONE',  ( 1.000000000000000000, -5.408326913195983465, -0.8000000000000000444 ) ) ;
#14629=ORIENTED_EDGE ( 'NONE', *, *, #8957, .F. ) ;
#14656=VECTOR ( 'NONE', #17746, 1000.000000000000000 ) ;
#14658=CARTESIAN_POINT ( 'NONE',  ( -0.1085714285714285687, -3.798448662927795372, -0.8000000000000000444 ) ) ;
#14663=DIRECTION ( 'NONE',  ( 0.000000000000000000, 0.000000000000000000, 1.000000000000000000 ) ) ;
#14668=DIRECTION ( 'NONE',  ( 1.000000000000000000, 0.000000000000000000, 0.000000000000000000 ) ) ;
#14669=ORIENTED_EDGE ( 'NONE', *, *, #16411, .T. ) ;
#14676=EDGE_CURVE ( 'NONE', #1031, #13632, #6556, .T. ) ;
#14692=ORIENTED_EDGE ( 'NONE', *, *, #1853, .T. ) ;
#14720=CYLINDRICAL_SURFACE ( 'NONE', #11718, 7.000000000000000000 ) ;
#14753=EDGE_CURVE ( 'NONE', #15143, #17997, #5181, .T. ) ;
#14757=ORIENTED_EDGE ( 'NONE', *, *, #14753, .F. ) ;
#14776=VERTEX_POINT ( 'NONE', #8022 ) ;
#14781=ORIENTED_EDGE ( 'NONE', *, *, #569, .T. ) ;
#14816=FACE_OUTER_BOUND ( 'NONE', #4697, .T. ) ;
#14819=FACE_OUTER_BOUND ( 'NONE', #6700, .T. ) ;
#14842=LINE ( 'NONE', #13371, #17445 ) ;
#14878=ORIENTED_EDGE ( 'NONE', *, *, #11670, .T. ) ;
#14879=ORIENTED_EDGE ( 'NONE', *, *, #7525, .F. ) ;
#14915=MANIFOLD_SOLID_BREP ( 'Notch', #12109 ) ;
#14933=VECTOR ( 'NONE', #4983, 1000.000000000000000 ) ;
#14958=ORIENTED_EDGE ( 'NONE', *, *, #5075, .F. ) ;
#14995=DIRECTION ( 'NONE',  ( 0.000000000000000000, 0.000000000000000000, 1.000000000000000000 ) ) ;
#15009=DIRECTION ( 'NONE',  ( -0.000000000000000000, -0.000000000000000000, -1.000000000000000000 ) ) ;
#15014=LINE ( 'NONE', #16499, #16510 ) ;
#15016=DIRECTION ( 'NONE',  ( 0.000000000000000000, 0.000000000000000000, 1.000000000000000000 ) ) ;
#15110=VECTOR ( 'NONE', #5833, 1000.000000000000000 ) ;
#15140=EDGE_CURVE ( 'NONE', #11712, #12595, #7338, .T. ) ;
#15143=VERTEX_POINT ( 'NONE', #11840 ) ;
#15150=DIRECTION ( 'NONE',  ( 1.000000000000000000, -0.000000000000000000, -0.000000000000000000 ) ) ;
#15171=ORIENTED_EDGE ( 'NONE', *, *, #11970, .T. ) ;
#15203=DIRECTION ( 'NONE',  ( 0.000000000000000000, 0.000000000000000000, 1.000000000000000000 ) ) ;
#15208=CYLINDRICAL_SURFACE ( 'NONE', #10228, 3.799999999999999378 ) ;
#15245=PLANE ( 'NONE',  #4084 ) ;
#15265=ORIENTED_EDGE ( 'NONE', *, *, #19126, .F. ) ;
#15286=ADVANCED_FACE ( 'NONE', ( #16057 ), #1147, .F. ) ;
#15300=VECTOR ( 'NONE', #16342, 1000.000000000000000 ) ;
#15314=CYLINDRICAL_SURFACE ( 'NONE', #1198, 0.5999999999999998668 ) ;
#15317=SURFACE_STYLE_USAGE ( .BOTH. , #9326 ) ;
#15328=CARTESIAN_POINT ( 'NONE',  ( 0.1085714285714285687, -3.798448662927795372, -0.8000000000000000444 ) ) ;
#15336=CARTESIAN_POINT ( 'NONE',  ( -1.000000000000000222, -4.808326913195983821, 0.000000000000000000 ) ) ;
#15390=CARTESIAN_POINT ( 'NONE',  ( 0.1085714285714285687, -3.798448662927795372, -0.8000000000000000444 ) ) ;
#15402=EDGE_CURVE ( 'NONE', #16449, #1031, #7121, .T. ) ;
#15420=DIRECTION ( 'NONE',  ( -0.000000000000000000, -0.000000000000000000, -1.000000000000000000 ) ) ;
#15433=VERTEX_POINT ( 'NONE', #4575 ) ;
#15468=DIRECTION ( 'NONE',  ( -0.000000000000000000, -0.000000000000000000, 1.000000000000000000 ) ) ;
#15472=CARTESIAN_POINT ( 'NONE',  ( 0.000000000000000000, 0.4273491293402468805, 0.000000000000000000 ) ) ;
#15495=DIRECTION ( 'NONE',  ( -0.000000000000000000, -0.000000000000000000, -1.000000000000000000 ) ) ;
#15514=DIRECTION ( 'NONE',  ( 0.000000000000000000, 0.000000000000000000, 1.000000000000000000 ) ) ;
#15535=ORIENTED_EDGE ( 'NONE', *, *, #406, .T. ) ;
#15579=ORIENTED_EDGE ( 'NONE', *, *, #10100, .F. ) ;
#15580=DIRECTION ( 'NONE',  ( 0.000000000000000000, 0.000000000000000000, 1.000000000000000000 ) ) ;
#15640=DIRECTION ( 'NONE',  ( 0.02857142857142857054, 0.9995917534020515305, 0.000000000000000000 ) ) ;
#15648=VECTOR ( 'NONE', #1393, 1000.000000000000114 ) ;
#15682=ORIENTED_EDGE ( 'NONE', *, *, #102, .T. ) ;
#15702=CARTESIAN_POINT ( 'NONE',  ( 3.799999999999999378, 0.000000000000000000, 0.000000000000000000 ) ) ;
#15712=DIRECTION ( 'NONE',  ( 0.000000000000000000, 0.000000000000000000, 1.000000000000000000 ) ) ;
#15725=DIRECTION ( 'NONE',  ( -0.000000000000000000, -0.000000000000000000, -1.000000000000000000 ) ) ;
#15728=VERTEX_POINT ( 'NONE', #10918 ) ;
#15733=VECTOR ( 'NONE', #9157, 1000.000000000000000 ) ;
#15746=DIRECTION ( 'NONE',  ( 1.000000000000000000, 0.000000000000000000, 0.000000000000000000 ) ) ;
#15757=PRODUCT_DEFINITION_FORMATION_WITH_SPECIFIED_SOURCE ( 'ANY', '', #14273, .NOT_KNOWN. ) ;
#15820=AXIS2_PLACEMENT_3D ( 'NONE', #6061, #1161, #5666 ) ;
#15834=EDGE_LOOP ( 'NONE', ( #8978, #18160, #10029, #18197 ) ) ;
#15876=AXIS2_PLACEMENT_3D ( 'NONE', #1805, #15514, #612 ) ;
#15886=EDGE_CURVE ( 'NONE', #12908, #7823, #14147, .T. ) ;
#15891=CIRCLE ( 'NONE', #17469, 0.5999999999999998668 ) ;
#15945=FACE_OUTER_BOUND ( 'NONE', #4881, .T. ) ;
#15956=COLOUR_RGB ( '',1.000000000000000000, 0.9490196078431372140, 0.9098039215686274384 ) ;
#15962=ORIENTED_EDGE ( 'NONE', *, *, #893, .T. ) ;
#15969=CARTESIAN_POINT ( 'NONE',  ( -2.321707774797442170, -4.824281976789052351, -0.8000000000000000444 ) ) ;
#16023=CARTESIAN_POINT ( 'NONE',  ( -2.321707774797442170, -4.824281976789052351, -0.8000000000000000444 ) ) ;
#16025=AXIS2_PLACEMENT_3D ( 'NONE', #7060, #14311, #2674 ) ;
#16039=CARTESIAN_POINT ( 'NONE',  ( 1.398397006336996817, -6.091550361990593743, -0.8000000000000000444 ) ) ;
#16057=FACE_OUTER_BOUND ( 'NONE', #11436, .T. ) ;
#16081=ORIENTED_EDGE ( 'NONE', *, *, #12958, .F. ) ;
#16084=ORIENTED_EDGE ( 'NONE', *, *, #10234, .F. ) ;
#16091=FACE_OUTER_BOUND ( 'NONE', #15834, .T. ) ;
#16146=DIRECTION ( 'NONE',  ( 1.000000000000000000, 0.000000000000000000, 0.000000000000000000 ) ) ;
#16148=ORIENTED_EDGE ( 'NONE', *, *, #9249, .F. ) ;
#16169=EDGE_CURVE ( 'NONE', #10416, #6867, #1615, .T. ) ;
#16191=DIRECTION ( 'NONE',  ( 1.000000000000000000, 0.000000000000000000, 0.000000000000000000 ) ) ;
#16211=CIRCLE ( 'NONE', #16527, 2.447112362156698140 ) ;
#16237=EDGE_CURVE ( 'NONE', #4109, #1031, #9711, .T. ) ;
#16249=CARTESIAN_POINT ( 'NONE',  ( -1.000000000000000222, -4.808326913195983821, -0.8000000000000000444 ) ) ;
#16306=AXIS2_PLACEMENT_3D ( 'NONE', #19125, #11639, #1068 ) ;
#16309=CARTESIAN_POINT ( 'NONE',  ( 3.160591952521659032, -3.281206521718069258, -0.8000000000000000444 ) ) ;
#16316=CARTESIAN_POINT ( 'NONE',  ( -0.1085714285714285687, -3.798448662927795372, -0.8000000000000000444 ) ) ;
#16342=DIRECTION ( 'NONE',  ( 0.1305261922200521840, 0.9914448613738103822, -0.000000000000000000 ) ) ;
#16411=EDGE_CURVE ( 'NONE', #7030, #8408, #19260, .T. ) ;
#16413=VERTEX_POINT ( 'NONE', #10006 ) ;
#16422=CARTESIAN_POINT ( 'NONE',  ( -1.000000000000000222, -4.808326913195983821, 0.000000000000000000 ) ) ;
#16424=CARTESIAN_POINT ( 'NONE',  ( 0.000000000000000000, 0.4273491293402468805, -0.8000000000000000444 ) ) ;
#16449=VERTEX_POINT ( 'NONE', #4143 ) ;
#16454=LINE ( 'NONE', #3309, #13225 ) ;
#16476=LINE ( 'NONE', #2395, #14933 ) ;
#16499=CARTESIAN_POINT ( 'NONE',  ( 0.9999999999999997780, -6.008326913195983998, 0.000000000000000000 ) ) ;
#16510=VECTOR ( 'NONE', #11868, 1000.000000000000000 ) ;
#16525=LINE ( 'NONE', #13757, #15733 ) ;
#16527=AXIS2_PLACEMENT_3D ( 'NONE', #5007, #15495, #18658 ) ;
#16567=ORIENTED_EDGE ( 'NONE', *, *, #14753, .T. ) ;
#16590=LINE ( 'NONE', #10399, #482 ) ;
#16591=EDGE_CURVE ( 'NONE', #18521, #10636, #20, .T. ) ;
#16598=EDGE_CURVE ( 'NONE', #9092, #13632, #4818, .T. ) ;
#16620=CIRCLE ( 'NONE', #8143, 3.799999999999999378 ) ;
#16621=DIRECTION ( 'NONE',  ( -0.000000000000000000, -0.000000000000000000, -1.000000000000000000 ) ) ;
#16635=ORIENTED_EDGE ( 'NONE', *, *, #8476, .T. ) ;
#16649=ORIENTED_EDGE ( 'NONE', *, *, #9172, .T. ) ;
#16661=VECTOR ( 'NONE', #8477, 1000.000000000000000 ) ;
#16662=EDGE_LOOP ( 'NONE', ( #4376, #12593, #4019, #10445 ) ) ;
#16678=CARTESIAN_POINT ( 'NONE',  ( 4.872650870659752442, 0.4273491293402468805, -0.8000000000000000444 ) ) ;
#16786=DIRECTION ( 'NONE',  ( 0.000000000000000000, 0.000000000000000000, 1.000000000000000000 ) ) ;
#16791=LINE ( 'NONE', #12559, #14082 ) ;
#16806=DIRECTION ( 'NONE',  ( 0.02857142857142857401, -0.9995917534020515305, 0.000000000000000000 ) ) ;
#16857=DIRECTION ( 'NONE',  ( 0.000000000000000000, 0.000000000000000000, 1.000000000000000000 ) ) ;
#16866=FACE_OUTER_BOUND ( 'NONE', #4407, .T. ) ;
#16880=AXIS2_PLACEMENT_3D ( 'NONE', #9954, #10058, #5454 ) ;
#16888=CARTESIAN_POINT ( 'NONE',  ( 0.1999999999999985678, -6.997142273814360713, -0.8000000000000000444 ) ) ;
#16920=VERTEX_POINT ( 'NONE', #5953 ) ;
#16929=PLANE ( 'NONE',  #14444 ) ;
#16936=FACE_OUTER_BOUND ( 'NONE', #6783, .T. ) ;
#16977=ORIENTED_EDGE ( 'NONE', *, *, #10347, .T. ) ;
#17013=DIRECTION ( 'NONE',  ( 0.000000000000000000, 0.000000000000000000, 1.000000000000000000 ) ) ;
#17035=DIRECTION ( 'NONE',  ( 0.000000000000000000, 0.000000000000000000, 1.000000000000000000 ) ) ;
#17078=CARTESIAN_POINT ( 'NONE',  ( 0.000000000000000000, 0.000000000000000000, -0.8000000000000000444 ) ) ;
#17095=VECTOR ( 'NONE', #8517, 1000.000000000000000 ) ;
#17121=FACE_OUTER_BOUND ( 'NONE', #7152, .T. ) ;
#17154=AXIS2_PLACEMENT_3D ( 'NONE', #12071, #10596, #6102 ) ;
#17171=CARTESIAN_POINT ( 'NONE',  ( -1.398397006336996817, -6.091550361990593743, 0.000000000000000000 ) ) ;
#17194=CARTESIAN_POINT ( 'NONE',  ( 0.1085714285714285687, -3.798448662927795372, 0.000000000000000000 ) ) ;
#17205=CARTESIAN_POINT ( 'NONE',  ( 0.000000000000000000, 0.000000000000000000, -0.8000000000000000444 ) ) ;
#17207=ORIENTED_EDGE ( 'NONE', *, *, #18997, .F. ) ;
#17314=CIRCLE ( 'NONE', #401, 4.872650870659752442 ) ;
#17356=ORIENTED_EDGE ( 'NONE', *, *, #6261, .T. ) ;
#17359=CARTESIAN_POINT ( 'NONE',  ( 1.000000000000000000, -6.008326913195983998, 0.000000000000000000 ) ) ;
#17403=ORIENTED_EDGE ( 'NONE', *, *, #12431, .F. ) ;
#17422=CIRCLE ( 'NONE', #500, 4.872650870659752442 ) ;
#17436=CARTESIAN_POINT ( 'NONE',  ( -1.000000000000000000, -5.408326913195983465, 0.000000000000000000 ) ) ;
#17445=VECTOR ( 'NONE', #5932, 1000.000000000000000 ) ;
#17463=ORIENTED_EDGE ( 'NONE', *, *, #4249, .T. ) ;
#17468=CARTESIAN_POINT ( 'NONE',  ( -2.321707774797442170, -4.824281976789052351, 0.000000000000000000 ) ) ;
#17469=AXIS2_PLACEMENT_3D ( 'NONE', #11867, #5804, #5900 ) ;
#17501=EDGE_CURVE ( 'NONE', #15433, #4109, #12140, .T. ) ;
#17589=VECTOR ( 'NONE', #6539, 1000.000000000000000 ) ;
#17592=CARTESIAN_POINT ( 'NONE',  ( 2.321707774797442170, -4.824281976789052351, 0.000000000000000000 ) ) ;
#17606=ORIENTED_EDGE ( 'NONE', *, *, #15886, .T. ) ;
#17617=CYLINDRICAL_SURFACE ( 'NONE', #6371, 0.7500000000000002220 ) ;
#17669=DIRECTION ( 'NONE',  ( 0.000000000000000000, 0.000000000000000000, 1.000000000000000000 ) ) ;
#17674=AXIS2_PLACEMENT_3D ( 'NONE', #12575, #15420, #6315 ) ;
#17715=CARTESIAN_POINT ( 'NONE',  ( -0.1374368770859597522, -4.808326913195983821, 0.000000000000000000 ) ) ;
#17725=DIRECTION ( 'NONE',  ( 0.000000000000000000, 0.000000000000000000, 1.000000000000000000 ) ) ;
#17745=CIRCLE ( 'NONE', #12072, 4.872650870659752442 ) ;
#17746=DIRECTION ( 'NONE',  ( -0.000000000000000000, -0.000000000000000000, 1.000000000000000000 ) ) ;
#17777=DIRECTION ( 'NONE',  ( -0.9995917534020515305, -0.02857142857142857054, 0.000000000000000000 ) ) ;
#17851=VERTEX_POINT ( 'NONE', #12571 ) ;
#17852=ADVANCED_FACE ( 'NONE', ( #14429 ), #12464, .T. ) ;
#17879=CARTESIAN_POINT ( 'NONE',  ( 0.000000000000000000, 0.000000000000000000, -0.8000000000000000444 ) ) ;
#17887=DIRECTION ( 'NONE',  ( 1.000000000000000000, 0.000000000000000000, 0.000000000000000000 ) ) ;
#17893=DIRECTION ( 'NONE',  ( 1.000000000000000000, 0.000000000000000000, 0.000000000000000000 ) ) ;
#17894=ORIENTED_EDGE ( 'NONE', *, *, #2152, .F. ) ;
#17924=EDGE_CURVE ( 'NONE', #1565, #17851, #2521, .T. ) ;
#17961=PLANE ( 'NONE',  #7073 ) ;
#17974=DIRECTION ( 'NONE',  ( 0.000000000000000000, 0.000000000000000000, 1.000000000000000000 ) ) ;
#17997=VERTEX_POINT ( 'NONE', #17592 ) ;
#18007=CARTESIAN_POINT ( 'NONE',  ( 0.1374368770859597522, -4.808326913195983821, 0.000000000000000000 ) ) ;
#18028=LINE ( 'NONE', #13211, #12364 ) ;
#18042=ADVANCED_FACE ( 'NONE', ( #14816 ), #1396, .T. ) ;
#18063=CARTESIAN_POINT ( 'NONE',  ( 1.599999999999999867, -5.408326913195983465, -0.8000000000000000444 ) ) ;
#18108=ORIENTED_EDGE ( 'NONE', *, *, #17924, .T. ) ;
#18125=CARTESIAN_POINT ( 'NONE',  ( 1.000000000000000000, -4.808326913195983821, -0.8000000000000000444 ) ) ;
#18147=CARTESIAN_POINT ( 'NONE',  ( 0.1085714285714285687, -3.798448662927795372, -0.8000000000000000444 ) ) ;
#18160=ORIENTED_EDGE ( 'NONE', *, *, #10836, .T. ) ;
#18197=ORIENTED_EDGE ( 'NONE', *, *, #9258, .F. ) ;
#18199=CARTESIAN_POINT ( 'NONE',  ( -0.1374368770859597522, -4.808326913195983821, -0.8000000000000000444 ) ) ;
#18211=ORIENTED_EDGE ( 'NONE', *, *, #1416, .T. ) ;
#18223=AXIS2_PLACEMENT_3D ( 'NONE', #14376, #11723, #14668 ) ;
#18300=ORIENTED_EDGE ( 'NONE', *, *, #19126, .T. ) ;
#18330=ADVANCED_FACE ( 'NONE', ( #15945 ), #1048, .T. ) ;
#18429=ORIENTED_EDGE ( 'NONE', *, *, #8449, .T. ) ;
#18463=DIRECTION ( 'NONE',  ( 0.000000000000000000, 0.000000000000000000, 1.000000000000000000 ) ) ;
#18521=VERTEX_POINT ( 'NONE', #17715 ) ;
#18564=CARTESIAN_POINT ( 'NONE',  ( 0.000000000000000000, 0.000000000000000000, -0.8000000000000000444 ) ) ;
#18573=FILL_AREA_STYLE ('',( #328 ) ) ;
#18600=CARTESIAN_POINT ( 'NONE',  ( 0.1085714285714285687, -3.798448662927795372, -0.8000000000000000444 ) ) ;
#18658=DIRECTION ( 'NONE',  ( 1.000000000000000000, 0.000000000000000000, 0.000000000000000000 ) ) ;
#18677=DIRECTION ( 'NONE',  ( 1.000000000000000000, 0.000000000000000000, 0.000000000000000000 ) ) ;
#18680=CYLINDRICAL_SURFACE ( 'NONE', #2565, 0.5999999999999999778 ) ;
#18694=ORIENTED_EDGE ( 'NONE', *, *, #13710, .F. ) ;
#18734=VERTEX_POINT ( 'NONE', #15336 ) ;
#18740=VECTOR ( 'NONE', #15580, 1000.000000000000000 ) ;
#18764=DIRECTION ( 'NONE',  ( 1.000000000000000000, 0.000000000000000000, 0.000000000000000000 ) ) ;
#18785=CARTESIAN_POINT ( 'NONE',  ( 4.872650870659752442, 0.4273491293402468805, 0.000000000000000000 ) ) ;
#18793=EDGE_LOOP ( 'NONE', ( #8311, #19112, #9236, #19229 ) ) ;
#18838=ORIENTED_EDGE ( 'NONE', *, *, #11970, .F. ) ;
#18903=EDGE_CURVE ( 'NONE', #7151, #3598, #16620, .T. ) ;
#18939=ORIENTED_EDGE ( 'NONE', *, *, #1976, .T. ) ;
#18940=ORIENTED_EDGE ( 'NONE', *, *, #2015, .F. ) ;
#18965=ORIENTED_EDGE ( 'NONE', *, *, #17501, .T. ) ;
#18970=DIRECTION ( 'NONE',  ( 1.000000000000000000, 0.000000000000000000, 0.000000000000000000 ) ) ;
#18972=CARTESIAN_POINT ( 'NONE',  ( -3.799999999999999378, 4.653657836759941744E-16, -0.8000000000000000444 ) ) ;
#18997=EDGE_CURVE ( 'NONE', #2159, #16413, #8471, .T. ) ;
#19053=CARTESIAN_POINT ( 'NONE',  ( -1.000000000000000000, -6.008326913195983998, 0.000000000000000000 ) ) ;
#19065=DIRECTION ( 'NONE',  ( 1.000000000000000000, 0.000000000000000000, -0.000000000000000000 ) ) ;
#19108=ORIENTED_EDGE ( 'NONE', *, *, #102, .F. ) ;
#19110=AXIS2_PLACEMENT_3D ( 'NONE', #2391, #6874, #12865 ) ;
#19112=ORIENTED_EDGE ( 'NONE', *, *, #7696, .F. ) ;
#19125=CARTESIAN_POINT ( 'NONE',  ( 0.000000000000000000, 0.000000000000000000, 0.000000000000000000 ) ) ;
#19126=EDGE_CURVE ( 'NONE', #3492, #8944, #5814, .T. ) ;
#19218=CYLINDRICAL_SURFACE ( 'NONE', #18223, 3.799999999999999378 ) ;
#19229=ORIENTED_EDGE ( 'NONE', *, *, #4838, .T. ) ;
#19260=LINE ( 'NONE', #2968, #15648 ) ;
#19275=DIRECTION ( 'NONE',  ( 0.02857142857142857401, 0.9995917534020515305, -0.000000000000000000 ) ) ;
#19285=LINE ( 'NONE', #16422, #5352 ) ;
#19302=ORIENTED_EDGE ( 'NONE', *, *, #406, .F. ) ;
#19328=ORIENTED_EDGE ( 'NONE', *, *, #15402, .F. ) ;
#19344=DIRECTION ( 'NONE',  ( 1.000000000000000000, 0.000000000000000000, 0.000000000000000000 ) ) ;
#19350=AXIS2_PLACEMENT_3D ( 'NONE', #16424, #3654, #13751 ) ;
#19352=DIRECTION ( 'NONE',  ( 1.000000000000000000, 0.000000000000000000, 0.000000000000000000 ) ) ;
#19368=DIRECTION ( 'NONE',  ( 0.000000000000000000, 0.000000000000000000, 1.000000000000000000 ) ) ;
#19381=DIRECTION ( 'NONE',  ( 0.000000000000000000, 0.000000000000000000, 1.000000000000000000 ) ) ;
#19385=DIRECTION ( 'NONE',  ( -1.000000000000000000, -0.000000000000000000, -0.000000000000000000 ) ) ;
#19398=CARTESIAN_POINT ( 'NONE',  ( 3.160591952521659032, -3.281206521718069258, -0.8000000000000000444 ) ) ;
#19462=COLOUR_RGB('Grey',0.48,0.52,0.57);
#19463=FILL_AREA_STYLE_COLOUR('',#19462);
#19464=FILL_AREA_STYLE('',(#19463));
#19465=SURFACE_STYLE_FILL_AREA(#19464);
#19466=SURFACE_SIDE_STYLE('',(#19465));
#19467=SURFACE_STYLE_USAGE(.BOTH.,#19466);
#19468=PRESENTATION_STYLE_ASSIGNMENT((#19467));
ENDSEC;
END-ISO-10303-21;
